ISO-10303-21;
HEADER;
/* Generated by software containing ST-Developer
 * from STEP Tools, Inc. (www.steptools.com) 
 */

FILE_DESCRIPTION(
/* description */ ('Independent compact industrial fixture table, bolted aluminum worktop
 on connected adjustable support base. Whole-mm nominal dimensions. No
 load rating assigned.'),
/* implementation_level */ '2;1');

FILE_NAME(
/* name */ 'Socket head cap screw M6x16.step',
/* time_stamp */ '2026-11-07T17:47:58-08:00',
/* author */ (''),
/* organization */ (''),
/* preprocessor_version */ 'ST-DEVELOPER v20.2',
/* originating_system */ 'Autodesk Translation Framework v15.17.0.0',
/* authorisation */ '');

FILE_SCHEMA (('AUTOMOTIVE_DESIGN { 1 0 10303 214 3 1 1 }'));
ENDSEC;

DATA;
#10=MECHANICAL_DESIGN_GEOMETRIC_PRESENTATION_REPRESENTATION('',(#2264),#97475);
#332=CONICAL_SURFACE('',#23023,2.5,0.785398163397448);
#360=B_SPLINE_SURFACE_WITH_KNOTS('',3,3,((#71871,#71872,#71873,#71874,#71875,
#71876,#71877,#71878,#71879,#71880,#71881,#71882,#71883,#71884,#71885,#71886,
#71887,#71888,#71889,#71890,#71891,#71892,#71893,#71894,#71895,#71896,#71897,
#71898,#71899,#71900,#71901,#71902,#71903,#71904,#71905,#71906,#71907,#71908,
#71909,#71910,#71911,#71912,#71913,#71914,#71915,#71916,#71917,#71918,#71919,
#71920,#71921,#71922,#71923,#71924,#71925,#71926,#71927,#71928,#71929,#71930,
#71931,#71932,#71933,#71934,#71935,#71936,#71937,#71938,#71939,#71940,#71941,
#71942,#71943,#71944,#71945,#71946,#71947,#71948,#71949,#71950,#71951,#71952,
#71953,#71954,#71955,#71956,#71957,#71958,#71959,#71960,#71961,#71962,#71963,
#71964,#71965,#71966,#71967,#71968,#71969,#71970,#71971,#71972),(#71973,
#71974,#71975,#71976,#71977,#71978,#71979,#71980,#71981,#71982,#71983,#71984,
#71985,#71986,#71987,#71988,#71989,#71990,#71991,#71992,#71993,#71994,#71995,
#71996,#71997,#71998,#71999,#72000,#72001,#72002,#72003,#72004,#72005,#72006,
#72007,#72008,#72009,#72010,#72011,#72012,#72013,#72014,#72015,#72016,#72017,
#72018,#72019,#72020,#72021,#72022,#72023,#72024,#72025,#72026,#72027,#72028,
#72029,#72030,#72031,#72032,#72033,#72034,#72035,#72036,#72037,#72038,#72039,
#72040,#72041,#72042,#72043,#72044,#72045,#72046,#72047,#72048,#72049,#72050,
#72051,#72052,#72053,#72054,#72055,#72056,#72057,#72058,#72059,#72060,#72061,
#72062,#72063,#72064,#72065,#72066,#72067,#72068,#72069,#72070,#72071,#72072,
#72073,#72074),(#72075,#72076,#72077,#72078,#72079,#72080,#72081,#72082,
#72083,#72084,#72085,#72086,#72087,#72088,#72089,#72090,#72091,#72092,#72093,
#72094,#72095,#72096,#72097,#72098,#72099,#72100,#72101,#72102,#72103,#72104,
#72105,#72106,#72107,#72108,#72109,#72110,#72111,#72112,#72113,#72114,#72115,
#72116,#72117,#72118,#72119,#72120,#72121,#72122,#72123,#72124,#72125,#72126,
#72127,#72128,#72129,#72130,#72131,#72132,#72133,#72134,#72135,#72136,#72137,
#72138,#72139,#72140,#72141,#72142,#72143,#72144,#72145,#72146,#72147,#72148,
#72149,#72150,#72151,#72152,#72153,#72154,#72155,#72156,#72157,#72158,#72159,
#72160,#72161,#72162,#72163,#72164,#72165,#72166,#72167,#72168,#72169,#72170,
#72171,#72172,#72173,#72174,#72175,#72176),(#72177,#72178,#72179,#72180,
#72181,#72182,#72183,#72184,#72185,#72186,#72187,#72188,#72189,#72190,#72191,
#72192,#72193,#72194,#72195,#72196,#72197,#72198,#72199,#72200,#72201,#72202,
#72203,#72204,#72205,#72206,#72207,#72208,#72209,#72210,#72211,#72212,#72213,
#72214,#72215,#72216,#72217,#72218,#72219,#72220,#72221,#72222,#72223,#72224,
#72225,#72226,#72227,#72228,#72229,#72230,#72231,#72232,#72233,#72234,#72235,
#72236,#72237,#72238,#72239,#72240,#72241,#72242,#72243,#72244,#72245,#72246,
#72247,#72248,#72249,#72250,#72251,#72252,#72253,#72254,#72255,#72256,#72257,
#72258,#72259,#72260,#72261,#72262,#72263,#72264,#72265,#72266,#72267,#72268,
#72269,#72270,#72271,#72272,#72273,#72274,#72275,#72276,#72277,#72278)),
 .UNSPECIFIED.,.F.,.F.,.F.,(4,4),(4,1,1,1,1,1,1,1,1,1,1,1,1,1,1,1,1,1,1,
1,1,1,1,1,1,1,1,1,1,1,1,1,1,1,1,1,1,1,1,1,1,1,1,1,1,1,1,1,1,1,1,1,1,1,1,
1,1,1,1,1,1,1,1,1,1,1,1,1,1,1,1,1,1,1,1,1,1,1,1,1,1,1,1,1,1,1,1,1,1,1,1,
1,1,1,1,1,1,1,1,4),(0.,0.0658467982010768),(11.6150328478182,12.6069034617266,
13.598774075635,14.5906446895433,15.5825153034517,16.5743859173601,17.5662565312685,
18.5581271451769,19.5499977590852,20.5418683729936,21.533738986902,22.5256096008104,
23.5174802147187,24.5093508286271,25.5012214425355,26.4930920564439,27.4849626703523,
28.4768332842606,29.468703898169,30.4605745120774,31.4524451259858,32.4443157398941,
33.4361863538025,34.4280569677109,35.4199275816193,36.4117981955277,37.403668809436,
38.3955394233444,39.3874100372528,40.3792806511612,41.3711512650695,42.3630218789779,
43.3548924928863,44.3467631067947,45.3386337207031,46.3305043346114,47.3223749485198,
48.3142455624282,49.3061161763366,50.2979867902449,51.2898574041533,52.2817280180617,
53.2735986319701,54.2654692458785,55.2573398597868,56.2492104736952,57.2410810876036,
58.232951701512,59.2248223154203,60.2166929293287,61.2085635432371,62.2004341571455,
63.1923047710539,64.1841753849622,65.1760459988706,66.167916612779,67.1597872266874,
68.1516578405957,69.1435284545041,70.1353990684125,71.1272696823209,72.1191402962293,
73.1110109101376,74.102881524046,75.0947521379544,76.0866227518628,77.0784933657711,
78.0703639796795,79.0622345935879,80.0541052074963,81.0459758214047,82.037846435313,
83.0297170492214,84.0215876631298,85.0134582770382,86.0053288909465,86.9971995048549,
87.9890701187633,88.9809407326717,89.9728113465801,90.9646819604884,91.9565525743968,
92.9484231883052,93.9402938022136,94.9321644161219,95.9240350300303,96.9159056439387,
97.9077762578471,98.8996468717555,99.8915174856638,100.883388099572,101.875258713481,
102.867129327389,103.858999941297,104.850870555206,105.842741169114,106.834611783022,
107.826482396931,108.818353010839,109.810223624748),.UNSPECIFIED.);
#361=B_SPLINE_SURFACE_WITH_KNOTS('',3,3,((#72407,#72408,#72409,#72410,#72411,
#72412,#72413,#72414,#72415,#72416,#72417,#72418,#72419,#72420,#72421,#72422,
#72423,#72424,#72425,#72426,#72427,#72428,#72429,#72430,#72431,#72432,#72433,
#72434,#72435,#72436,#72437,#72438,#72439,#72440,#72441,#72442,#72443,#72444,
#72445,#72446,#72447,#72448,#72449,#72450,#72451,#72452,#72453,#72454,#72455,
#72456,#72457,#72458,#72459,#72460,#72461,#72462,#72463,#72464,#72465,#72466,
#72467,#72468,#72469,#72470,#72471,#72472,#72473,#72474,#72475,#72476,#72477,
#72478,#72479,#72480,#72481,#72482,#72483,#72484,#72485,#72486,#72487,#72488,
#72489,#72490,#72491,#72492,#72493,#72494,#72495,#72496,#72497,#72498,#72499,
#72500,#72501,#72502,#72503,#72504,#72505,#72506,#72507,#72508,#72509,#72510),
(#72511,#72512,#72513,#72514,#72515,#72516,#72517,#72518,#72519,#72520,
#72521,#72522,#72523,#72524,#72525,#72526,#72527,#72528,#72529,#72530,#72531,
#72532,#72533,#72534,#72535,#72536,#72537,#72538,#72539,#72540,#72541,#72542,
#72543,#72544,#72545,#72546,#72547,#72548,#72549,#72550,#72551,#72552,#72553,
#72554,#72555,#72556,#72557,#72558,#72559,#72560,#72561,#72562,#72563,#72564,
#72565,#72566,#72567,#72568,#72569,#72570,#72571,#72572,#72573,#72574,#72575,
#72576,#72577,#72578,#72579,#72580,#72581,#72582,#72583,#72584,#72585,#72586,
#72587,#72588,#72589,#72590,#72591,#72592,#72593,#72594,#72595,#72596,#72597,
#72598,#72599,#72600,#72601,#72602,#72603,#72604,#72605,#72606,#72607,#72608,
#72609,#72610,#72611,#72612,#72613,#72614),(#72615,#72616,#72617,#72618,
#72619,#72620,#72621,#72622,#72623,#72624,#72625,#72626,#72627,#72628,#72629,
#72630,#72631,#72632,#72633,#72634,#72635,#72636,#72637,#72638,#72639,#72640,
#72641,#72642,#72643,#72644,#72645,#72646,#72647,#72648,#72649,#72650,#72651,
#72652,#72653,#72654,#72655,#72656,#72657,#72658,#72659,#72660,#72661,#72662,
#72663,#72664,#72665,#72666,#72667,#72668,#72669,#72670,#72671,#72672,#72673,
#72674,#72675,#72676,#72677,#72678,#72679,#72680,#72681,#72682,#72683,#72684,
#72685,#72686,#72687,#72688,#72689,#72690,#72691,#72692,#72693,#72694,#72695,
#72696,#72697,#72698,#72699,#72700,#72701,#72702,#72703,#72704,#72705,#72706,
#72707,#72708,#72709,#72710,#72711,#72712,#72713,#72714,#72715,#72716,#72717,
#72718),(#72719,#72720,#72721,#72722,#72723,#72724,#72725,#72726,#72727,
#72728,#72729,#72730,#72731,#72732,#72733,#72734,#72735,#72736,#72737,#72738,
#72739,#72740,#72741,#72742,#72743,#72744,#72745,#72746,#72747,#72748,#72749,
#72750,#72751,#72752,#72753,#72754,#72755,#72756,#72757,#72758,#72759,#72760,
#72761,#72762,#72763,#72764,#72765,#72766,#72767,#72768,#72769,#72770,#72771,
#72772,#72773,#72774,#72775,#72776,#72777,#72778,#72779,#72780,#72781,#72782,
#72783,#72784,#72785,#72786,#72787,#72788,#72789,#72790,#72791,#72792,#72793,
#72794,#72795,#72796,#72797,#72798,#72799,#72800,#72801,#72802,#72803,#72804,
#72805,#72806,#72807,#72808,#72809,#72810,#72811,#72812,#72813,#72814,#72815,
#72816,#72817,#72818,#72819,#72820,#72821,#72822)),.UNSPECIFIED.,.F.,.F.,
 .F.,(4,4),(4,1,1,1,1,1,1,1,1,1,1,1,1,1,1,1,1,1,1,1,1,1,1,1,1,1,1,1,1,1,
1,1,1,1,1,1,1,1,1,1,1,1,1,1,1,1,1,1,1,1,1,1,1,1,1,1,1,1,1,1,1,1,1,1,1,1,
1,1,1,1,1,1,1,1,1,1,1,1,1,1,1,1,1,1,1,1,1,1,1,1,1,1,1,1,1,1,1,1,1,1,1,4),
(0.,0.0658467982010768),(8.30747755240101,9.30018873014199,10.292899907883,
11.2856110856239,12.2783222633649,13.2710334411059,14.2637446188469,15.2564557965878,
16.2491669743288,17.2418781520698,18.2345893298108,19.2273005075518,20.2200116852927,
21.2127228630337,22.2054340407747,23.1981452185157,24.1908563962566,25.1835675739976,
26.1762787517386,27.1689899294796,28.1617011072206,29.1544122849615,30.1471234627025,
31.1398346404435,32.1325458181845,33.1252569959254,34.1179681736664,35.1106793514074,
36.1033905291484,37.0961017068893,38.0888128846303,39.0815240623713,40.0742352401123,
41.0669464178533,42.0596575955942,43.0523687733352,44.0450799510762,45.0377911288172,
46.0305023065581,47.0232134842991,48.0159246620401,49.0086358397811,50.001347017522,
50.994058195263,51.986769373004,52.979480550745,53.972191728486,54.9649029062269,
55.9576140839679,56.9503252617089,57.9430364394499,58.9357476171908,59.9284587949318,
60.9211699726728,61.9138811504138,62.9065923281547,63.8993035058957,64.8920146836367,
65.8847258613777,66.8774370391187,67.8701482168596,68.8628593946006,69.8555705723416,
70.8482817500825,71.8409929278235,72.8337041055645,73.8264152833055,74.8191264610465,
75.8118376387874,76.8045488165284,77.7972599942694,78.7899711720104,79.7826823497514,
80.7753935274923,81.7681047052333,82.7608158829743,83.7535270607153,84.7462382384562,
85.7389494161972,86.7316605939382,87.7243717716792,88.7170829494201,89.7097941271611,
90.7025053049021,91.6952164826431,92.687927660384,93.680638838125,94.673350015866,
95.666061193607,96.658772371348,97.6514835490889,98.6441947268299,99.6369059045709,
100.629617082312,101.622328260053,102.615039437794,103.607750615535,104.600461793276,
105.593172971017,106.585884148758,107.578595326499,108.57130650424),
 .UNSPECIFIED.);
#1410=B_SPLINE_CURVE_WITH_KNOTS('',3,(#70463,#70464,#70465,#70466,#70467,
#70468,#70469,#70470,#70471,#70472),.UNSPECIFIED.,.F.,.F.,(4,3,3,4),(-4.09293042013066,
-3.96748245563351,-2.97561184172513,-2.06863817490915),.UNSPECIFIED.);
#1411=B_SPLINE_CURVE_WITH_KNOTS('',3,(#70475,#70476,#70477,#70478,#70479,
#70480,#70481),.UNSPECIFIED.,.F.,.F.,(4,3,4),(0.,0.992711177740983,1.1173004083682),
 .UNSPECIFIED.);
#1412=B_SPLINE_CURVE_WITH_KNOTS('',3,(#70486,#70487,#70488,#70489,#70490,
#70491,#70492,#70493,#70494,#70495,#70496,#70497,#70498,#70499,#70500,#70501,
#70502,#70503,#70504,#70505,#70506,#70507),.UNSPECIFIED.,.F.,.F.,(4,3,3,
3,3,3,3,4),(-10.3761157273102,-9.91870613908378,-8.9268355251754,-7.93496491126702,
-6.94309429735864,-5.95122368345026,-4.95935306954189,-4.09293042013066),
 .UNSPECIFIED.);
#1413=B_SPLINE_CURVE_WITH_KNOTS('',3,(#70508,#70509,#70510,#70511,#70512,
#70513,#70514,#70515,#70516,#70517,#70518,#70519,#70520,#70521,#70522,#70523,
#70524,#70525,#70526,#70527,#70528,#70529),.UNSPECIFIED.,.F.,.F.,(4,3,3,
3,3,3,3,4),(1.1173004083682,1.98542235548196,2.97813353322293,3.97084471096391,
4.96355588870488,5.95626706644586,6.94897824418683,7.40048571554779),
 .UNSPECIFIED.);
#1414=B_SPLINE_CURVE_WITH_KNOTS('',3,(#70534,#70535,#70536,#70537,#70538,
#70539,#70540,#70541,#70542,#70543,#70544,#70545,#70546,#70547,#70548,#70549,
#70550,#70551,#70552,#70553,#70554,#70555),.UNSPECIFIED.,.F.,.F.,(4,3,3,
3,3,3,3,4),(-16.6593010344898,-15.869929822534,-14.8780592086257,-13.8861885947173,
-12.8943179808089,-11.9024473669005,-10.9105767529922,-10.3761157273102),
 .UNSPECIFIED.);
#1415=B_SPLINE_CURVE_WITH_KNOTS('',3,(#70556,#70557,#70558,#70559,#70560,
#70561,#70562,#70563,#70564,#70565,#70566,#70567,#70568,#70569,#70570,#70571,
#70572,#70573,#70574,#70575,#70576,#70577),.UNSPECIFIED.,.F.,.F.,(4,3,3,
3,3,3,3,4),(7.40048571554779,7.94168942192781,8.93440059966879,9.92711177740977,
10.9198229551507,11.9125341328917,12.9052453106327,13.6836710227274),
 .UNSPECIFIED.);
#1416=B_SPLINE_CURVE_WITH_KNOTS('',3,(#70582,#70583,#70584,#70585,#70586,
#70587,#70588,#70589,#70590,#70591,#70592,#70593,#70594,#70595,#70596,#70597,
#70598,#70599,#70600,#70601,#70602,#70603,#70604,#70605,#70606),
 .UNSPECIFIED.,.F.,.F.,(4,3,3,3,3,3,3,3,4),(-22.9424863416694,-22.8130241198927,
-21.8211535059843,-20.8292828920759,-19.8374122781676,-18.8455416642592,
-17.8536710503508,-16.8618004364424,-16.6593010344898),.UNSPECIFIED.);
#1417=B_SPLINE_CURVE_WITH_KNOTS('',3,(#70607,#70608,#70609,#70610,#70611,
#70612,#70613,#70614,#70615,#70616,#70617,#70618,#70619,#70620,#70621,#70622,
#70623,#70624,#70625,#70626,#70627,#70628,#70629,#70630,#70631),
 .UNSPECIFIED.,.F.,.F.,(4,3,3,3,3,3,3,3,4),(13.6836710227274,13.8979564883737,
14.8906676661147,15.8833788438556,16.8760900215966,17.8688011993376,18.8615123770786,
19.8542235548195,19.966856329907),.UNSPECIFIED.);
#1418=B_SPLINE_CURVE_WITH_KNOTS('',3,(#70636,#70637,#70638,#70639,#70640,
#70641,#70642,#70643,#70644,#70645,#70646,#70647,#70648,#70649,#70650,#70651,
#70652,#70653,#70654,#70655,#70656,#70657),.UNSPECIFIED.,.F.,.F.,(4,3,3,
3,3,3,3,4),(-29.225671648849,-28.764247803343,-27.7723771894346,-26.7805065755262,
-25.7886359616178,-24.7967653477094,-23.8048947338011,-22.9424863416694),
 .UNSPECIFIED.);
#1419=B_SPLINE_CURVE_WITH_KNOTS('',3,(#70658,#70659,#70660,#70661,#70662,
#70663,#70664,#70665,#70666,#70667,#70668,#70669,#70670,#70671,#70672,#70673,
#70674,#70675,#70676,#70677,#70678,#70679),.UNSPECIFIED.,.F.,.F.,(4,3,3,
3,3,3,3,4),(19.966856329907,20.8469347325605,21.8396459103015,22.8323570880425,
23.8250682657834,24.8177794435244,25.8104906212654,26.2500416370865),
 .UNSPECIFIED.);
#1420=B_SPLINE_CURVE_WITH_KNOTS('',3,(#70684,#70685,#70686,#70687,#70688,
#70689,#70690,#70691,#70692,#70693,#70694,#70695,#70696,#70697,#70698,#70699,
#70700,#70701,#70702,#70703,#70704,#70705),.UNSPECIFIED.,.F.,.F.,(4,3,3,
3,3,3,3,4),(-35.5088569560286,-34.7154714867932,-33.7236008728848,-32.7317302589765,
-31.7398596450681,-30.7479890311597,-29.7561184172513,-29.225671648849),
 .UNSPECIFIED.);
#1421=B_SPLINE_CURVE_WITH_KNOTS('',3,(#70706,#70707,#70708,#70709,#70710,
#70711,#70712,#70713,#70714,#70715,#70716,#70717,#70718,#70719,#70720,#70721,
#70722,#70723,#70724,#70725,#70726,#70727),.UNSPECIFIED.,.F.,.F.,(4,3,3,
3,3,3,3,4),(26.2500416370865,26.8032017990064,27.7959129767474,28.7886241544883,
29.7813353322293,30.7740465099703,31.7667576877113,32.5332269442661),
 .UNSPECIFIED.);
#1422=B_SPLINE_CURVE_WITH_KNOTS('',3,(#70732,#70733,#70734,#70735,#70736,
#70737,#70738,#70739,#70740,#70741,#70742,#70743,#70744,#70745,#70746,#70747,
#70748,#70749,#70750,#70751,#70752,#70753,#70754,#70755,#70756),
 .UNSPECIFIED.,.F.,.F.,(4,3,3,3,3,3,3,3,4),(-41.7920422632082,-41.6585657841519,
-40.6666951702435,-39.6748245563351,-38.6829539424267,-37.6910833285184,
-36.69921271461,-35.7073421007016,-35.5088569560286),.UNSPECIFIED.);
#1423=B_SPLINE_CURVE_WITH_KNOTS('',3,(#70757,#70758,#70759,#70760,#70761,
#70762,#70763,#70764,#70765,#70766,#70767,#70768,#70769,#70770,#70771,#70772,
#70773,#70774,#70775,#70776,#70777,#70778,#70779,#70780,#70781),
 .UNSPECIFIED.,.F.,.F.,(4,3,3,3,3,3,3,3,4),(32.5332269442661,32.7594688654522,
33.7521800431932,34.7448912209342,35.7376023986752,36.7303135764161,37.7230247541571,
38.7157359318981,38.8164122514457),.UNSPECIFIED.);
#1424=B_SPLINE_CURVE_WITH_KNOTS('',3,(#70786,#70787,#70788,#70789,#70790,
#70791,#70792,#70793,#70794,#70795,#70796,#70797,#70798,#70799,#70800,#70801,
#70802,#70803,#70804,#70805,#70806,#70807),.UNSPECIFIED.,.F.,.F.,(4,3,3,
3,3,3,3,4),(-48.0752275703878,-47.6097894676021,-46.6179188536938,-45.6260482397854,
-44.634177625877,-43.6423070119686,-42.6504363980602,-41.7920422632082),
 .UNSPECIFIED.);
#1425=B_SPLINE_CURVE_WITH_KNOTS('',3,(#70808,#70809,#70810,#70811,#70812,
#70813,#70814,#70815,#70816,#70817,#70818,#70819,#70820,#70821,#70822,#70823,
#70824,#70825,#70826,#70827,#70828,#70829),.UNSPECIFIED.,.F.,.F.,(4,3,3,
3,3,3,3,4),(38.8164122514457,39.7084471096391,40.7011582873801,41.693869465121,
42.686580642862,43.679291820603,44.672002998344,45.0995975586253),
 .UNSPECIFIED.);
#1426=B_SPLINE_CURVE_WITH_KNOTS('',3,(#70834,#70835,#70836,#70837,#70838,
#70839,#70840,#70841,#70842,#70843,#70844,#70845,#70846,#70847,#70848,#70849,
#70850,#70851,#70852,#70853,#70854,#70855),.UNSPECIFIED.,.F.,.F.,(4,3,3,
3,3,3,3,4),(-54.3584128775674,-53.5610131510524,-52.569142537144,-51.5772719232356,
-50.5854013093273,-49.5935306954189,-48.6016600815105,-48.0752275703878),
 .UNSPECIFIED.);
#1427=B_SPLINE_CURVE_WITH_KNOTS('',3,(#70856,#70857,#70858,#70859,#70860,
#70861,#70862,#70863,#70864,#70865,#70866,#70867,#70868,#70869,#70870,#70871,
#70872,#70873,#70874,#70875,#70876,#70877),.UNSPECIFIED.,.F.,.F.,(4,3,3,
3,3,3,3,4),(45.0995975586253,45.6647141760849,46.6574253538259,47.6501365315669,
48.6428477093079,49.6355588870488,50.6282700647898,51.3827828658049),
 .UNSPECIFIED.);
#1428=B_SPLINE_CURVE_WITH_KNOTS('',3,(#70882,#70883,#70884,#70885,#70886,
#70887,#70888,#70889,#70890,#70891,#70892,#70893,#70894,#70895,#70896,#70897,
#70898,#70899,#70900,#70901,#70902,#70903,#70904,#70905,#70906),
 .UNSPECIFIED.,.F.,.F.,(4,3,3,3,3,3,3,3,4),(-60.641598184747,-60.5041074484111,
-59.5122368345027,-58.5203662205943,-57.5284956066859,-56.5366249927775,
-55.5447543788692,-54.5528837649608,-54.3584128775674),.UNSPECIFIED.);
#1429=B_SPLINE_CURVE_WITH_KNOTS('',3,(#70907,#70908,#70909,#70910,#70911,
#70912,#70913,#70914,#70915,#70916,#70917,#70918,#70919,#70920,#70921,#70922,
#70923,#70924,#70925,#70926,#70927,#70928,#70929,#70930,#70931),
 .UNSPECIFIED.,.F.,.F.,(4,3,3,3,3,3,3,3,4),(51.3827828658049,51.6209812425308,
52.6136924202718,53.6064035980127,54.5991147757537,55.5918259534947,56.5845371312357,
57.5772483089767,57.6659681729845),.UNSPECIFIED.);
#1430=B_SPLINE_CURVE_WITH_KNOTS('',3,(#70936,#70937,#70938,#70939,#70940,
#70941,#70942,#70943,#70944,#70945,#70946,#70947,#70948,#70949,#70950,#70951,
#70952,#70953,#70954,#70955,#70956,#70957),.UNSPECIFIED.,.F.,.F.,(4,3,3,
3,3,3,3,4),(-66.9247834919266,-66.4553311318613,-65.4634605179529,-64.4715899040445,
-63.4797192901362,-62.4878486762278,-61.4959780623194,-60.641598184747),
 .UNSPECIFIED.);
#1431=B_SPLINE_CURVE_WITH_KNOTS('',3,(#70958,#70959,#70960,#70961,#70962,
#70963,#70964,#70965,#70966,#70967,#70968,#70969,#70970,#70971,#70972,#70973,
#70974,#70975,#70976,#70977,#70978,#70979),.UNSPECIFIED.,.F.,.F.,(4,3,3,
3,3,3,3,4),(57.6659681729845,58.5699594867177,59.5626706644586,60.5553818421996,
61.5480930199406,62.5408041976816,63.5335153754225,63.9491534801641),
 .UNSPECIFIED.);
#1432=B_SPLINE_CURVE_WITH_KNOTS('',3,(#70984,#70985,#70986,#70987,#70988,
#70989,#70990,#70991,#70992,#70993,#70994,#70995,#70996,#70997,#70998,#70999,
#71000,#71001,#71002,#71003,#71004,#71005),.UNSPECIFIED.,.F.,.F.,(4,3,3,
3,3,3,3,4),(-73.2079687991062,-72.4065548153116,-71.4146842014032,-70.4228135874948,
-69.4309429735864,-68.4390723596781,-67.4472017457697,-66.9247834919266),
 .UNSPECIFIED.);
#1433=B_SPLINE_CURVE_WITH_KNOTS('',3,(#71006,#71007,#71008,#71009,#71010,
#71011,#71012,#71013,#71014,#71015,#71016,#71017,#71018,#71019,#71020,#71021,
#71022,#71023,#71024,#71025,#71026,#71027),.UNSPECIFIED.,.F.,.F.,(4,3,3,
3,3,3,3,4),(63.9491534801641,64.5262265531635,65.5189377309045,66.5116489086455,
67.5043600863864,68.4970712641274,69.4897824418684,70.2323387873437),
 .UNSPECIFIED.);
#1434=B_SPLINE_CURVE_WITH_KNOTS('',3,(#71032,#71033,#71034,#71035,#71036,
#71037,#71038,#71039,#71040,#71041,#71042,#71043,#71044,#71045,#71046,#71047,
#71048,#71049,#71050,#71051,#71052,#71053,#71054,#71055,#71056),
 .UNSPECIFIED.,.F.,.F.,(4,3,3,3,3,3,3,3,4),(-79.4911541062857,-79.3496491126702,
-78.3577784987618,-77.3659078848535,-76.3740372709451,-75.3821666570367,
-74.3902960431283,-73.3984254292199,-73.2079687991062),.UNSPECIFIED.);
#1435=B_SPLINE_CURVE_WITH_KNOTS('',3,(#71057,#71058,#71059,#71060,#71061,
#71062,#71063,#71064,#71065,#71066,#71067,#71068,#71069,#71070,#71071,#71072,
#71073,#71074,#71075,#71076,#71077,#71078,#71079,#71080,#71081),
 .UNSPECIFIED.,.F.,.F.,(4,3,3,3,3,3,3,3,4),(70.2323387873437,70.4824936196094,
71.4752047973503,72.4679159750913,73.4606271528323,74.4533383305733,75.4460495083142,
76.4387606860552,76.5155240945233),.UNSPECIFIED.);
#1436=B_SPLINE_CURVE_WITH_KNOTS('',3,(#71086,#71087,#71088,#71089,#71090,
#71091,#71092,#71093,#71094,#71095,#71096,#71097,#71098,#71099,#71100,#71101,
#71102,#71103,#71104,#71105,#71106,#71107),.UNSPECIFIED.,.F.,.F.,(4,3,3,
3,3,3,3,4),(-85.7743394134653,-85.3008727961205,-84.3090021822121,-83.3171315683037,
-82.3252609543953,-81.333390340487,-80.3415197265786,-79.4911541062857),
 .UNSPECIFIED.);
#1437=B_SPLINE_CURVE_WITH_KNOTS('',3,(#71108,#71109,#71110,#71111,#71112,
#71113,#71114,#71115,#71116,#71117,#71118,#71119,#71120,#71121,#71122,#71123,
#71124,#71125,#71126,#71127,#71128,#71129),.UNSPECIFIED.,.F.,.F.,(4,3,3,
3,3,3,3,4),(76.5155240945233,77.4314718637962,78.4241830415372,79.4168942192782,
80.4096053970191,81.4023165747601,82.3950277525011,82.7987094017029),
 .UNSPECIFIED.);
#1438=B_SPLINE_CURVE_WITH_KNOTS('',3,(#71134,#71135,#71136,#71137,#71138,
#71139,#71140,#71141,#71142,#71143,#71144,#71145,#71146,#71147,#71148,#71149,
#71150,#71151,#71152,#71153,#71154,#71155),.UNSPECIFIED.,.F.,.F.,(4,3,3,
3,3,3,3,4),(-92.0575247206449,-91.2520964795708,-90.2602258656624,-89.268355251754,
-88.2764846378456,-87.2846140239373,-86.2927434100289,-85.7743394134653),
 .UNSPECIFIED.);
#1439=B_SPLINE_CURVE_WITH_KNOTS('',3,(#71156,#71157,#71158,#71159,#71160,
#71161,#71162,#71163,#71164,#71165,#71166,#71167,#71168,#71169,#71170,#71171,
#71172,#71173,#71174,#71175,#71176,#71177),.UNSPECIFIED.,.F.,.F.,(4,3,3,
3,3,3,3,4),(82.7987094017029,83.3877389302421,84.380450107983,85.373161285724,
86.365872463465,87.358583641206,88.351294818947,89.0818947088825),
 .UNSPECIFIED.);
#1440=B_SPLINE_CURVE_WITH_KNOTS('',3,(#71183,#71184,#71185,#71186,#71187,
#71188,#71189,#71190,#71191,#71192),.UNSPECIFIED.,.F.,.F.,(4,1,1,1,1,1,
1,4),(103.672557568463,103.858999941297,104.850870555206,105.842741169114,
106.834611783022,107.826482396931,108.818353010839,109.810223624748),
 .UNSPECIFIED.);
#1441=B_SPLINE_CURVE_WITH_KNOTS('',3,(#71195,#71196,#71197,#71198,#71199,
#71200,#71201,#71202),.UNSPECIFIED.,.F.,.F.,(4,1,1,1,1,4),(103.672557568463,
104.600461793276,105.593172971017,106.585884148758,107.578595326499,108.57130650424),
 .UNSPECIFIED.);
#1442=B_SPLINE_CURVE_WITH_KNOTS('',3,(#71207,#71208,#71209,#71210,#71211,
#71212,#71213,#71214,#71215,#71216),.UNSPECIFIED.,.F.,.F.,(4,1,1,1,1,1,
1,4),(97.3893722612836,97.9077762578471,98.8996468717555,99.8915174856638,
100.883388099572,101.875258713481,102.867129327389,103.672557568463),
 .UNSPECIFIED.);
#1443=B_SPLINE_CURVE_WITH_KNOTS('',3,(#71217,#71218,#71219,#71220,#71221,
#71222,#71223,#71224,#71225,#71226,#71227),.UNSPECIFIED.,.F.,.F.,(4,1,1,
1,1,1,1,1,4),(97.3893722612836,97.6514835490889,98.6441947268299,99.6369059045709,
100.629617082312,101.622328260053,102.615039437794,103.607750615535,103.672557568463),
 .UNSPECIFIED.);
#1444=B_SPLINE_CURVE_WITH_KNOTS('',3,(#71232,#71233,#71234,#71235,#71236,
#71237,#71238,#71239,#71240,#71241),.UNSPECIFIED.,.F.,.F.,(4,1,1,1,1,1,
1,4),(91.106186954104,91.9565525743968,92.9484231883052,93.9402938022136,
94.9321644161219,95.9240350300303,96.9159056439387,97.3893722612836),
 .UNSPECIFIED.);
#1445=B_SPLINE_CURVE_WITH_KNOTS('',3,(#71242,#71243,#71244,#71245,#71246,
#71247,#71248,#71249,#71250,#71251),.UNSPECIFIED.,.F.,.F.,(4,1,1,1,1,1,
1,4),(91.106186954104,91.6952164826431,92.687927660384,93.680638838125,
94.673350015866,95.666061193607,96.658772371348,97.3893722612836),
 .UNSPECIFIED.);
#1446=B_SPLINE_CURVE_WITH_KNOTS('',3,(#71256,#71257,#71258,#71259,#71260,
#71261,#71262,#71263,#71264,#71265,#71266),.UNSPECIFIED.,.F.,.F.,(4,1,1,
1,1,1,1,1,4),(84.8230016469244,85.0134582770382,86.0053288909465,86.9971995048549,
87.9890701187633,88.9809407326717,89.9728113465801,90.9646819604884,91.106186954104),
 .UNSPECIFIED.);
#1447=B_SPLINE_CURVE_WITH_KNOTS('',3,(#71267,#71268,#71269,#71270,#71271,
#71272,#71273,#71274,#71275,#71276),.UNSPECIFIED.,.F.,.F.,(4,1,1,1,1,1,
1,4),(84.8230016469244,85.7389494161972,86.7316605939382,87.7243717716792,
88.7170829494201,89.7097941271611,90.7025053049021,91.106186954104),
 .UNSPECIFIED.);
#1448=B_SPLINE_CURVE_WITH_KNOTS('',3,(#71281,#71282,#71283,#71284,#71285,
#71286,#71287,#71288,#71289,#71290),.UNSPECIFIED.,.F.,.F.,(4,1,1,1,1,1,
1,4),(78.5398163397448,79.0622345935879,80.0541052074963,81.0459758214047,
82.037846435313,83.0297170492214,84.0215876631298,84.8230016469244),
 .UNSPECIFIED.);
#1449=B_SPLINE_CURVE_WITH_KNOTS('',3,(#71291,#71292,#71293,#71294,#71295,
#71296,#71297,#71298,#71299,#71300,#71301),.UNSPECIFIED.,.F.,.F.,(4,1,1,
1,1,1,1,1,4),(78.5398163397448,78.7899711720104,79.7826823497514,80.7753935274923,
81.7681047052333,82.7608158829743,83.7535270607153,84.7462382384562,84.8230016469244),
 .UNSPECIFIED.);
#1450=B_SPLINE_CURVE_WITH_KNOTS('',3,(#71306,#71307,#71308,#71309,#71310,
#71311,#71312,#71313,#71314,#71315),.UNSPECIFIED.,.F.,.F.,(4,1,1,1,1,1,
1,4),(72.2566310325652,73.1110109101376,74.102881524046,75.0947521379544,
76.0866227518628,77.0784933657711,78.0703639796795,78.5398163397448),
 .UNSPECIFIED.);
#1451=B_SPLINE_CURVE_WITH_KNOTS('',3,(#71316,#71317,#71318,#71319,#71320,
#71321,#71322,#71323,#71324,#71325),.UNSPECIFIED.,.F.,.F.,(4,1,1,1,1,1,
1,4),(72.2566310325652,72.8337041055645,73.8264152833055,74.8191264610465,
75.8118376387874,76.8045488165284,77.7972599942694,78.5398163397448),
 .UNSPECIFIED.);
#1452=B_SPLINE_CURVE_WITH_KNOTS('',3,(#71330,#71331,#71332,#71333,#71334,
#71335,#71336,#71337,#71338,#71339,#71340),.UNSPECIFIED.,.F.,.F.,(4,1,1,
1,1,1,1,1,4),(65.9734457253856,66.167916612779,67.1597872266874,68.1516578405957,
69.1435284545041,70.1353990684125,71.1272696823209,72.1191402962293,72.2566310325652),
 .UNSPECIFIED.);
#1453=B_SPLINE_CURVE_WITH_KNOTS('',3,(#71341,#71342,#71343,#71344,#71345,
#71346,#71347,#71348,#71349,#71350),.UNSPECIFIED.,.F.,.F.,(4,1,1,1,1,1,
1,4),(65.9734457253856,66.8774370391187,67.8701482168596,68.8628593946006,
69.8555705723416,70.8482817500825,71.8409929278235,72.2566310325652),
 .UNSPECIFIED.);
#1454=B_SPLINE_CURVE_WITH_KNOTS('',3,(#71355,#71356,#71357,#71358,#71359,
#71360,#71361,#71362,#71363,#71364),.UNSPECIFIED.,.F.,.F.,(4,1,1,1,1,1,
1,4),(59.6902604182061,60.2166929293287,61.2085635432371,62.2004341571455,
63.1923047710539,64.1841753849622,65.1760459988706,65.9734457253856),
 .UNSPECIFIED.);
#1455=B_SPLINE_CURVE_WITH_KNOTS('',3,(#71365,#71366,#71367,#71368,#71369,
#71370,#71371,#71372,#71373,#71374,#71375),.UNSPECIFIED.,.F.,.F.,(4,1,1,
1,1,1,1,1,4),(59.690260418206,59.9284587949318,60.9211699726728,61.9138811504138,
62.9065923281547,63.8993035058957,64.8920146836367,65.8847258613777,65.9734457253856),
 .UNSPECIFIED.);
#1456=B_SPLINE_CURVE_WITH_KNOTS('',3,(#71380,#71381,#71382,#71383,#71384,
#71385,#71386,#71387,#71388,#71389),.UNSPECIFIED.,.F.,.F.,(4,1,1,1,1,1,
1,4),(53.4070751110265,54.2654692458785,55.2573398597868,56.2492104736952,
57.2410810876036,58.232951701512,59.2248223154203,59.6902604182061),
 .UNSPECIFIED.);
#1457=B_SPLINE_CURVE_WITH_KNOTS('',3,(#71390,#71391,#71392,#71393,#71394,
#71395,#71396,#71397,#71398,#71399),.UNSPECIFIED.,.F.,.F.,(4,1,1,1,1,1,
1,4),(53.4070751110264,53.972191728486,54.9649029062269,55.9576140839679,
56.9503252617089,57.9430364394499,58.9357476171908,59.690260418206),
 .UNSPECIFIED.);
#1458=B_SPLINE_CURVE_WITH_KNOTS('',3,(#71404,#71405,#71406,#71407,#71408,
#71409,#71410,#71411,#71412,#71413,#71414),.UNSPECIFIED.,.F.,.F.,(4,1,1,
1,1,1,1,1,4),(47.1238898038469,47.3223749485198,48.3142455624282,49.3061161763366,
50.2979867902449,51.2898574041533,52.2817280180617,53.2735986319701,53.4070751110265),
 .UNSPECIFIED.);
#1459=B_SPLINE_CURVE_WITH_KNOTS('',3,(#71415,#71416,#71417,#71418,#71419,
#71420,#71421,#71422,#71423,#71424),.UNSPECIFIED.,.F.,.F.,(4,1,1,1,1,1,
1,4),(47.1238898038468,48.0159246620401,49.0086358397811,50.001347017522,
50.994058195263,51.986769373004,52.979480550745,53.4070751110264),
 .UNSPECIFIED.);
#1460=B_SPLINE_CURVE_WITH_KNOTS('',3,(#71429,#71430,#71431,#71432,#71433,
#71434,#71435,#71436,#71437,#71438),.UNSPECIFIED.,.F.,.F.,(4,1,1,1,1,1,
1,4),(40.8407044966673,41.3711512650695,42.3630218789779,43.3548924928863,
44.3467631067947,45.3386337207031,46.3305043346114,47.1238898038469),
 .UNSPECIFIED.);
#1461=B_SPLINE_CURVE_WITH_KNOTS('',3,(#71439,#71440,#71441,#71442,#71443,
#71444,#71445,#71446,#71447,#71448,#71449),.UNSPECIFIED.,.F.,.F.,(4,1,1,
1,1,1,1,1,4),(40.8407044966672,41.0669464178533,42.0596575955942,43.0523687733352,
44.0450799510762,45.0377911288172,46.0305023065581,47.0232134842991,47.1238898038468),
 .UNSPECIFIED.);
#1462=B_SPLINE_CURVE_WITH_KNOTS('',3,(#71454,#71455,#71456,#71457,#71458,
#71459,#71460,#71461,#71462,#71463),.UNSPECIFIED.,.F.,.F.,(4,1,1,1,1,1,
1,4),(34.5575191894877,35.4199275816193,36.4117981955277,37.403668809436,
38.3955394233444,39.3874100372528,40.3792806511612,40.8407044966673),
 .UNSPECIFIED.);
#1463=B_SPLINE_CURVE_WITH_KNOTS('',3,(#71464,#71465,#71466,#71467,#71468,
#71469,#71470,#71471,#71472,#71473),.UNSPECIFIED.,.F.,.F.,(4,1,1,1,1,1,
1,4),(34.5575191894876,35.1106793514074,36.1033905291484,37.0961017068893,
38.0888128846303,39.0815240623713,40.0742352401123,40.8407044966672),
 .UNSPECIFIED.);
#1464=B_SPLINE_CURVE_WITH_KNOTS('',3,(#71478,#71479,#71480,#71481,#71482,
#71483,#71484,#71485,#71486,#71487,#71488),.UNSPECIFIED.,.F.,.F.,(4,1,1,
1,1,1,1,1,4),(28.2743338823081,28.4768332842606,29.468703898169,30.4605745120774,
31.4524451259858,32.4443157398941,33.4361863538025,34.4280569677109,34.5575191894877),
 .UNSPECIFIED.);
#1465=B_SPLINE_CURVE_WITH_KNOTS('',3,(#71489,#71490,#71491,#71492,#71493,
#71494,#71495,#71496,#71497,#71498),.UNSPECIFIED.,.F.,.F.,(4,1,1,1,1,1,
1,4),(28.2743338823081,29.1544122849615,30.1471234627025,31.1398346404435,
32.1325458181845,33.1252569959254,34.1179681736664,34.5575191894876),
 .UNSPECIFIED.);
#1466=B_SPLINE_CURVE_WITH_KNOTS('',3,(#71503,#71504,#71505,#71506,#71507,
#71508,#71509,#71510,#71511,#71512),.UNSPECIFIED.,.F.,.F.,(4,1,1,1,1,1,
1,4),(21.9911485751285,22.5256096008104,23.5174802147187,24.5093508286271,
25.5012214425355,26.4930920564439,27.4849626703523,28.2743338823081),
 .UNSPECIFIED.);
#1467=B_SPLINE_CURVE_WITH_KNOTS('',3,(#71513,#71514,#71515,#71516,#71517,
#71518,#71519,#71520,#71521,#71522,#71523),.UNSPECIFIED.,.F.,.F.,(4,1,1,
1,1,1,1,1,4),(21.9911485751285,22.2054340407747,23.1981452185157,24.1908563962566,
25.1835675739976,26.1762787517386,27.1689899294796,28.1617011072206,28.2743338823081),
 .UNSPECIFIED.);
#1468=B_SPLINE_CURVE_WITH_KNOTS('',3,(#71528,#71529,#71530,#71531,#71532,
#71533,#71534,#71535,#71536,#71537),.UNSPECIFIED.,.F.,.F.,(4,1,1,1,1,1,
1,4),(15.7079632679489,16.5743859173601,17.5662565312685,18.5581271451769,
19.5499977590852,20.5418683729936,21.533738986902,21.9911485751285),
 .UNSPECIFIED.);
#1469=B_SPLINE_CURVE_WITH_KNOTS('',3,(#71538,#71539,#71540,#71541,#71542,
#71543,#71544,#71545,#71546,#71547),.UNSPECIFIED.,.F.,.F.,(4,1,1,1,1,1,
1,4),(15.7079632679489,16.2491669743288,17.2418781520698,18.2345893298108,
19.2273005075518,20.2200116852927,21.2127228630337,21.9911485751285),
 .UNSPECIFIED.);
#1470=B_SPLINE_CURVE_WITH_KNOTS('',3,(#71550,#71551,#71552,#71553,#71554,
#71555,#71556,#71557,#71558,#71559,#71560,#71561,#71562,#71563,#71564,#71565,
#71566,#71567,#71568,#71569,#71570,#71571,#71572,#71573,#71574,#71575,#71576,
#71577,#71578,#71579,#71580,#71581,#71582,#71583,#71584,#71585,#71586,#71587,
#71588,#71589,#71590,#71591,#71592,#71593,#71594,#71595,#71596,#71597,#71598,
#71599,#71600,#71601,#71602,#71603,#71604,#71605,#71606,#71607,#71608,#71609,
#71610,#71611,#71612,#71613,#71614,#71615,#71616,#71617,#71618,#71619,#71620,
#71621,#71622,#71623,#71624,#71625,#71626,#71627,#71628,#71629,#71630,#71631,
#71632,#71633,#71634,#71635,#71636,#71637,#71638,#71639,#71640,#71641,#71642,
#71643,#71644,#71645,#71646,#71647,#71648,#71649,#71650,#71651,#71652,#71653,
#71654,#71655,#71656,#71657,#71658,#71659,#71660,#71661,#71662,#71663,#71664,
#71665,#71666,#71667,#71668,#71669,#71670,#71671,#71672,#71673,#71674,#71675,
#71676,#71677,#71678,#71679,#71680,#71681,#71682,#71683,#71684,#71685,#71686,
#71687,#71688,#71689,#71690,#71691,#71692,#71693,#71694,#71695,#71696,#71697,
#71698,#71699,#71700,#71701,#71702,#71703,#71704,#71705,#71706,#71707,#71708,
#71709,#71710,#71711,#71712,#71713,#71714,#71715,#71716,#71717,#71718,#71719,
#71720,#71721,#71722,#71723,#71724,#71725,#71726,#71727,#71728,#71729,#71730,
#71731,#71732,#71733,#71734,#71735,#71736,#71737,#71738,#71739,#71740,#71741,
#71742,#71743,#71744,#71745,#71746,#71747,#71748,#71749,#71750,#71751,#71752,
#71753,#71754,#71755,#71756,#71757,#71758,#71759,#71760,#71761,#71762,#71763,
#71764,#71765,#71766,#71767,#71768,#71769),.UNSPECIFIED.,.F.,.F.,(4,3,3,
3,3,3,3,3,3,3,3,3,3,3,3,3,3,3,3,3,3,3,3,3,3,3,3,3,3,3,3,3,3,3,3,3,3,3,3,
3,3,3,3,3,3,3,3,3,3,3,3,3,3,3,3,3,3,3,3,3,3,3,3,3,3,3,3,3,3,3,3,3,3,4),
(-1.5115530493723,-1.48679433039677,-1.46137997144481,-1.44936627203976,
-1.44203978844916,-1.43723948275662,-1.41130482704604,-1.3851425648951,
-1.36907979899106,-1.36528335260342,-1.33883417182409,-1.31251413265359,
-1.29083745680875,-1.27999911888633,-1.27252822943752,-1.26916078096391,
-1.2438409010096,-1.21777622976252,-1.19264806966918,-1.18165449962834,
-1.17500808302858,-1.17140113753098,-1.14461626345551,-1.11752388424601,
-1.09233065043846,-1.08197947093734,-1.07663416157974,-1.07221334700158,
-1.04448214800868,-1.01675094901579,-0.989899829038698,-0.980534050538336,
-0.975142748268706,-0.971473262423844,-0.944367339171939,-0.916829945945447,
-0.889160172398661,-0.878253059899969,-0.87283587922991,-0.869128423226553,
-0.840502786522066,-0.812629809126308,-0.785184824902654,-0.776260550181423,
-0.769615191493828,-0.76539079696697,-0.754625876408607,-0.727617533495154,
-0.699889836956671,-0.672733437279935,-0.663027286995113,-0.658922109894078,
-0.630659562625353,-0.602060824740566,-0.57220527844112,-0.560770556686858,
-0.556383058918736,-0.552005977862112,-0.523133364911618,-0.494697204184849,
-0.482638639542781,-0.454174910522506,-0.448377858002803,-0.443883394073885,
-0.415482165359649,-0.386508614853008,-0.357316612716015,-0.340170191390177,
-0.335377465438287,-0.305918315871394,-0.27645436453335,-0.247645675491356,
-0.226999958751525,-0.219677966288016),.UNSPECIFIED.);
#1471=B_SPLINE_CURVE_WITH_KNOTS('',3,(#71771,#71772,#71773,#71774,#71775,
#71776,#71777,#71778,#71779,#71780,#71781,#71782,#71783,#71784,#71785,#71786,
#71787,#71788,#71789,#71790,#71791,#71792,#71793,#71794,#71795,#71796,#71797,
#71798,#71799,#71800,#71801,#71802,#71803,#71804,#71805,#71806,#71807,#71808,
#71809,#71810,#71811,#71812,#71813,#71814,#71815,#71816,#71817,#71818,#71819,
#71820,#71821,#71822,#71823,#71824,#71825,#71826,#71827,#71828,#71829,#71830,
#71831,#71832,#71833,#71834),.UNSPECIFIED.,.F.,.F.,(4,3,3,3,3,3,3,3,3,3,
3,3,3,3,3,3,3,3,3,3,3,4),(-0.410648750433038,-0.381296088292737,-0.350882391849445,
-0.328072119516976,-0.310964415267624,-0.305842993500878,-0.301661871504881,
-0.274116258800685,-0.259641302519569,-0.231392457082299,-0.202468399947011,
-0.198019208917011,-0.170841895434807,-0.143725312403613,-0.117042212888725,
-0.102411936277635,-0.097195049751494,-0.0935363835720784,-0.0677899334604712,
-0.0424347820407558,-0.0178142542830924,0.),.UNSPECIFIED.);
#1472=B_SPLINE_CURVE_WITH_KNOTS('',3,(#71837,#71838,#71839,#71840,#71841,
#71842,#71843,#71844,#71845,#71846,#71847,#71848,#71849,#71850,#71851,#71852,
#71853,#71854,#71855,#71856,#71857,#71858,#71859,#71860,#71861,#71862,#71863,
#71864,#71865,#71866,#71867),.UNSPECIFIED.,.F.,.F.,(4,3,3,3,3,3,3,3,3,3,
4),(-0.219677966288016,-0.201006229477425,-0.172158028090248,-0.142713390739092,
-0.124874216896705,-0.114789665948937,-0.110082687886506,-0.0803547102951982,
-0.0502957032480209,-0.0203907630638487,0.),.UNSPECIFIED.);
#1473=B_SPLINE_CURVE_WITH_KNOTS('',3,(#72280,#72281,#72282,#72283,#72284,
#72285,#72286,#72287),.UNSPECIFIED.,.F.,.F.,(4,1,1,1,1,4),(11.6150328478182,
12.6069034617266,13.598774075635,14.5906446895433,15.5825153034517,15.7079632679489),
 .UNSPECIFIED.);
#1474=B_SPLINE_CURVE_WITH_KNOTS('',3,(#72288,#72289,#72290,#72291,#72292,
#72293,#72294,#72295,#72296,#72297,#72298,#72299,#72300,#72301,#72302,#72303,
#72304,#72305,#72306,#72307,#72308,#72309,#72310,#72311,#72312,#72313,#72314,
#72315,#72316,#72317,#72318,#72319,#72320,#72321,#72322,#72323,#72324,#72325,
#72326,#72327,#72328,#72329,#72330,#72331,#72332,#72333,#72334,#72335,#72336,
#72337,#72338,#72339,#72340,#72341,#72342,#72343,#72344,#72345,#72346,#72347,
#72348,#72349,#72350,#72351,#72352,#72353,#72354,#72355,#72356,#72357,#72358,
#72359,#72360,#72361,#72362,#72363,#72364,#72365,#72366,#72367,#72368,#72369,
#72370,#72371,#72372,#72373,#72374,#72375),.UNSPECIFIED.,.F.,.F.,(4,3,3,
3,3,3,3,3,3,3,3,3,3,3,3,3,3,3,3,3,3,3,3,3,3,3,3,3,3,4),(-0.552745378375041,
-0.527830263536694,-0.498419933292456,-0.482944277728704,-0.477004703287069,
-0.471889411648522,-0.442842142020847,-0.418838054802294,-0.408336266644177,
-0.40199148464016,-0.397446251891128,-0.369139848009071,-0.341087780585202,
-0.313931322984348,-0.298150853306366,-0.293754274173184,-0.266922432864957,
-0.250809444272419,-0.223433348051691,-0.19550417954523,-0.19139998392206,
-0.164790719651446,-0.138164593558308,-0.11192170155777,-0.0979314888630491,
-0.0936568444848153,-0.0680692021908508,-0.0428602319276656,-0.0184469101431373,
0.),.UNSPECIFIED.);
#1475=B_SPLINE_CURVE_WITH_KNOTS('',3,(#72376,#72377,#72378,#72379,#72380,
#72381,#72382,#72383,#72384,#72385,#72386,#72387,#72388,#72389,#72390,#72391,
#72392,#72393,#72394),.UNSPECIFIED.,.F.,.F.,(4,3,3,3,3,3,4),(-96.6808425304193,
-96.2114495491126,-95.2195789352043,-94.2277083212959,-93.2358377073875,
-92.2439670934791,-92.0575247206449),.UNSPECIFIED.);
#1476=B_SPLINE_CURVE_WITH_KNOTS('',3,(#72397,#72398,#72399,#72400,#72401,
#72402,#72403,#72404,#72405),.UNSPECIFIED.,.F.,.F.,(4,1,1,1,1,1,4),(10.3761157273101,
11.2856110856239,12.2783222633649,13.2710334411059,14.2637446188469,15.2564557965878,
15.7079632679489),.UNSPECIFIED.);
#1477=B_SPLINE_CURVE_WITH_KNOTS('',3,(#72823,#72824,#72825,#72826,#72827,
#72828,#72829,#72830,#72831,#72832,#72833,#72834,#72835,#72836,#72837,#72838,
#72839,#72840,#72841,#72842,#72843,#72844),.UNSPECIFIED.,.F.,.F.,(4,3,3,
3,3,3,3,4),(89.0818947088825,89.3440059966879,90.3367171744289,91.3294283521699,
92.3221395299109,93.3148507076518,94.3075618853928,94.6122043555102),
 .UNSPECIFIED.);
#1478=B_SPLINE_CURVE_WITH_KNOTS('',3,(#72845,#72846,#72847,#72848,#72849,
#72850,#72851,#72852,#72853,#72854,#72855,#72856,#72857,#72858,#72859,#72860,
#72861,#72862,#72863,#72864,#72865,#72866,#72867,#72868,#72869,#72870,#72871,
#72872,#72873,#72874,#72875,#72876,#72877,#72878,#72879,#72880,#72881,#72882,
#72883,#72884,#72885,#72886,#72887,#72888,#72889,#72890,#72891,#72892,#72893,
#72894,#72895,#72896,#72897,#72898,#72899,#72900,#72901,#72902,#72903,#72904,
#72905,#72906,#72907,#72908,#72909,#72910,#72911,#72912,#72913,#72914,#72915,
#72916,#72917,#72918,#72919,#72920,#72921,#72922,#72923,#72924,#72925,#72926,
#72927,#72928,#72929,#72930,#72931,#72932),.UNSPECIFIED.,.F.,.F.,(4,3,3,
3,3,3,3,3,3,3,3,3,3,3,3,3,3,3,3,3,3,3,3,3,3,3,3,3,3,4),(-0.555272788399392,
-0.535208229286056,-0.51046000550438,-0.495927663091087,-0.490771565699598,
-0.464551573131573,-0.44160907963455,-0.431518091480653,-0.425427657470475,
-0.420791193383041,-0.394188077983384,-0.365893964776387,-0.344673379871139,
-0.328757941192203,-0.324434111993057,-0.296521822210165,-0.281011625155395,
-0.254049889550291,-0.226554106924644,-0.220947145848259,-0.216688100237889,
-0.188737539857684,-0.160250957640402,-0.131525362881473,-0.114279480489655,
-0.109581292141837,-0.0801117384511396,-0.0505679692714886,-0.0215915474943119,
0.),.UNSPECIFIED.);
#2226=SHAPE_REPRESENTATION_RELATIONSHIP('SRR','None',#97620,#2245);
#2245=ADVANCED_BREP_SHAPE_REPRESENTATION('',(#2283),#97470);
#2264=STYLED_ITEM('',(#97720),#2283);
#2283=MANIFOLD_SOLID_BREP('Body1',#21825);
#2359=FACE_BOUND('',#4521,.T.);
#2360=FACE_BOUND('',#4524,.T.);
#2507=PLANE('',#23029);
#2508=PLANE('',#23030);
#2509=PLANE('',#23031);
#2510=PLANE('',#23032);
#2511=PLANE('',#23033);
#2512=PLANE('',#23034);
#2513=PLANE('',#23035);
#2514=PLANE('',#23036);
#2515=PLANE('',#23040);
#2516=PLANE('',#23041);
#3253=FACE_OUTER_BOUND('',#4478,.T.);
#3254=FACE_OUTER_BOUND('',#4479,.T.);
#3255=FACE_OUTER_BOUND('',#4480,.T.);
#3256=FACE_OUTER_BOUND('',#4481,.T.);
#3257=FACE_OUTER_BOUND('',#4482,.T.);
#3258=FACE_OUTER_BOUND('',#4483,.T.);
#3259=FACE_OUTER_BOUND('',#4484,.T.);
#3260=FACE_OUTER_BOUND('',#4485,.T.);
#3261=FACE_OUTER_BOUND('',#4486,.T.);
#3262=FACE_OUTER_BOUND('',#4487,.T.);
#3263=FACE_OUTER_BOUND('',#4488,.T.);
#3264=FACE_OUTER_BOUND('',#4489,.T.);
#3265=FACE_OUTER_BOUND('',#4490,.T.);
#3266=FACE_OUTER_BOUND('',#4491,.T.);
#3267=FACE_OUTER_BOUND('',#4492,.T.);
#3268=FACE_OUTER_BOUND('',#4493,.T.);
#3269=FACE_OUTER_BOUND('',#4494,.T.);
#3270=FACE_OUTER_BOUND('',#4495,.T.);
#3271=FACE_OUTER_BOUND('',#4496,.T.);
#3272=FACE_OUTER_BOUND('',#4497,.T.);
#3273=FACE_OUTER_BOUND('',#4498,.T.);
#3274=FACE_OUTER_BOUND('',#4499,.T.);
#3275=FACE_OUTER_BOUND('',#4500,.T.);
#3276=FACE_OUTER_BOUND('',#4501,.T.);
#3277=FACE_OUTER_BOUND('',#4502,.T.);
#3278=FACE_OUTER_BOUND('',#4503,.T.);
#3279=FACE_OUTER_BOUND('',#4504,.T.);
#3280=FACE_OUTER_BOUND('',#4505,.T.);
#3281=FACE_OUTER_BOUND('',#4506,.T.);
#3282=FACE_OUTER_BOUND('',#4507,.T.);
#3283=FACE_OUTER_BOUND('',#4508,.T.);
#3284=FACE_OUTER_BOUND('',#4509,.T.);
#3285=FACE_OUTER_BOUND('',#4510,.T.);
#3286=FACE_OUTER_BOUND('',#4511,.T.);
#3287=FACE_OUTER_BOUND('',#4512,.T.);
#3288=FACE_OUTER_BOUND('',#4513,.T.);
#3289=FACE_OUTER_BOUND('',#4514,.T.);
#3290=FACE_OUTER_BOUND('',#4515,.T.);
#3291=FACE_OUTER_BOUND('',#4516,.T.);
#3292=FACE_OUTER_BOUND('',#4517,.T.);
#3293=FACE_OUTER_BOUND('',#4518,.T.);
#3294=FACE_OUTER_BOUND('',#4519,.T.);
#3295=FACE_OUTER_BOUND('',#4520,.T.);
#3296=FACE_OUTER_BOUND('',#4522,.T.);
#3297=FACE_OUTER_BOUND('',#4523,.T.);
#3298=FACE_OUTER_BOUND('',#4525,.T.);
#4478=EDGE_LOOP('',(#17166,#17167,#17168,#17169));
#4479=EDGE_LOOP('',(#17170,#17171,#17172,#17173));
#4480=EDGE_LOOP('',(#17174,#17175,#17176,#17177));
#4481=EDGE_LOOP('',(#17178,#17179,#17180,#17181));
#4482=EDGE_LOOP('',(#17182,#17183,#17184,#17185));
#4483=EDGE_LOOP('',(#17186,#17187,#17188,#17189));
#4484=EDGE_LOOP('',(#17190,#17191,#17192,#17193));
#4485=EDGE_LOOP('',(#17194,#17195,#17196,#17197));
#4486=EDGE_LOOP('',(#17198,#17199,#17200,#17201));
#4487=EDGE_LOOP('',(#17202,#17203,#17204,#17205));
#4488=EDGE_LOOP('',(#17206,#17207,#17208,#17209));
#4489=EDGE_LOOP('',(#17210,#17211,#17212,#17213));
#4490=EDGE_LOOP('',(#17214,#17215,#17216,#17217));
#4491=EDGE_LOOP('',(#17218,#17219,#17220,#17221));
#4492=EDGE_LOOP('',(#17222,#17223,#17224,#17225));
#4493=EDGE_LOOP('',(#17226,#17227,#17228,#17229));
#4494=EDGE_LOOP('',(#17230,#17231,#17232,#17233));
#4495=EDGE_LOOP('',(#17234,#17235,#17236,#17237));
#4496=EDGE_LOOP('',(#17238,#17239,#17240,#17241));
#4497=EDGE_LOOP('',(#17242,#17243,#17244,#17245));
#4498=EDGE_LOOP('',(#17246,#17247,#17248,#17249));
#4499=EDGE_LOOP('',(#17250,#17251,#17252,#17253));
#4500=EDGE_LOOP('',(#17254,#17255,#17256,#17257));
#4501=EDGE_LOOP('',(#17258,#17259,#17260,#17261));
#4502=EDGE_LOOP('',(#17262,#17263,#17264,#17265));
#4503=EDGE_LOOP('',(#17266,#17267,#17268,#17269));
#4504=EDGE_LOOP('',(#17270,#17271,#17272,#17273));
#4505=EDGE_LOOP('',(#17274,#17275,#17276,#17277));
#4506=EDGE_LOOP('',(#17278,#17279,#17280,#17281));
#4507=EDGE_LOOP('',(#17282,#17283,#17284,#17285));
#4508=EDGE_LOOP('',(#17286,#17287,#17288,#17289,#17290,#17291,#17292,#17293));
#4509=EDGE_LOOP('',(#17294,#17295,#17296,#17297,#17298,#17299,#17300,#17301,
#17302,#17303,#17304,#17305,#17306,#17307,#17308,#17309,#17310,#17311,#17312,
#17313,#17314,#17315,#17316,#17317,#17318,#17319,#17320,#17321,#17322,#17323,
#17324,#17325,#17326,#17327));
#4510=EDGE_LOOP('',(#17328,#17329,#17330,#17331));
#4511=EDGE_LOOP('',(#17332,#17333,#17334,#17335,#17336,#17337,#17338,#17339,
#17340,#17341,#17342,#17343,#17344,#17345,#17346,#17347,#17348,#17349,#17350,
#17351,#17352,#17353,#17354,#17355,#17356,#17357,#17358,#17359,#17360,#17361,
#17362,#17363,#17364,#17365,#17366));
#4512=EDGE_LOOP('',(#17367,#17368,#17369,#17370));
#4513=EDGE_LOOP('',(#17371,#17372,#17373,#17374));
#4514=EDGE_LOOP('',(#17375,#17376,#17377,#17378));
#4515=EDGE_LOOP('',(#17379,#17380,#17381,#17382));
#4516=EDGE_LOOP('',(#17383,#17384,#17385,#17386));
#4517=EDGE_LOOP('',(#17387,#17388,#17389,#17390));
#4518=EDGE_LOOP('',(#17391,#17392,#17393,#17394));
#4519=EDGE_LOOP('',(#17395,#17396,#17397,#17398,#17399,#17400));
#4520=EDGE_LOOP('',(#17401));
#4521=EDGE_LOOP('',(#17402,#17403,#17404,#17405));
#4522=EDGE_LOOP('',(#17406,#17407,#17408,#17409));
#4523=EDGE_LOOP('',(#17410));
#4524=EDGE_LOOP('',(#17411,#17412,#17413,#17414,#17415,#17416));
#4525=EDGE_LOOP('',(#17417));
#5726=LINE('',#70461,#6940);
#5727=LINE('',#70485,#6941);
#5728=LINE('',#70533,#6942);
#5729=LINE('',#70581,#6943);
#5730=LINE('',#70635,#6944);
#5731=LINE('',#70683,#6945);
#5732=LINE('',#70731,#6946);
#5733=LINE('',#70785,#6947);
#5734=LINE('',#70833,#6948);
#5735=LINE('',#70881,#6949);
#5736=LINE('',#70935,#6950);
#5737=LINE('',#70983,#6951);
#5738=LINE('',#71031,#6952);
#5739=LINE('',#71085,#6953);
#5740=LINE('',#71133,#6954);
#5741=LINE('',#71181,#6955);
#5742=LINE('',#71206,#6956);
#5743=LINE('',#71231,#6957);
#5744=LINE('',#71255,#6958);
#5745=LINE('',#71280,#6959);
#5746=LINE('',#71305,#6960);
#5747=LINE('',#71329,#6961);
#5748=LINE('',#71354,#6962);
#5749=LINE('',#71379,#6963);
#5750=LINE('',#71403,#6964);
#5751=LINE('',#71428,#6965);
#5752=LINE('',#71453,#6966);
#5753=LINE('',#71477,#6967);
#5754=LINE('',#71502,#6968);
#5755=LINE('',#71527,#6969);
#5756=LINE('',#71869,#6970);
#5757=LINE('',#72937,#6971);
#5758=LINE('',#72939,#6972);
#5759=LINE('',#72941,#6973);
#5760=LINE('',#72942,#6974);
#5761=LINE('',#72945,#6975);
#5762=LINE('',#72947,#6976);
#5763=LINE('',#72948,#6977);
#5764=LINE('',#72951,#6978);
#5765=LINE('',#72953,#6979);
#5766=LINE('',#72954,#6980);
#5767=LINE('',#72957,#6981);
#5768=LINE('',#72959,#6982);
#5769=LINE('',#72960,#6983);
#5770=LINE('',#72963,#6984);
#5771=LINE('',#72965,#6985);
#5772=LINE('',#72966,#6986);
#5773=LINE('',#72968,#6987);
#5774=LINE('',#72969,#6988);
#5775=LINE('',#72976,#6989);
#6940=VECTOR('',#26196,3.);
#6941=VECTOR('',#26201,3.);
#6942=VECTOR('',#26204,3.);
#6943=VECTOR('',#26207,3.);
#6944=VECTOR('',#26210,3.);
#6945=VECTOR('',#26213,3.);
#6946=VECTOR('',#26216,3.);
#6947=VECTOR('',#26219,3.);
#6948=VECTOR('',#26222,3.);
#6949=VECTOR('',#26225,3.);
#6950=VECTOR('',#26228,3.);
#6951=VECTOR('',#26231,3.);
#6952=VECTOR('',#26234,3.);
#6953=VECTOR('',#26237,3.);
#6954=VECTOR('',#26240,3.);
#6955=VECTOR('',#26243,2.37175);
#6956=VECTOR('',#26248,2.37175);
#6957=VECTOR('',#26251,2.37175);
#6958=VECTOR('',#26254,2.37175);
#6959=VECTOR('',#26257,2.37175);
#6960=VECTOR('',#26260,2.37175);
#6961=VECTOR('',#26263,2.37175);
#6962=VECTOR('',#26266,2.37175);
#6963=VECTOR('',#26269,2.37175);
#6964=VECTOR('',#26272,2.37175);
#6965=VECTOR('',#26275,2.37175);
#6966=VECTOR('',#26278,2.37175);
#6967=VECTOR('',#26281,2.37175);
#6968=VECTOR('',#26284,2.37175);
#6969=VECTOR('',#26287,2.37175);
#6970=VECTOR('',#26292,2.5);
#6971=VECTOR('',#26303,10.);
#6972=VECTOR('',#26304,10.);
#6973=VECTOR('',#26305,10.);
#6974=VECTOR('',#26306,10.);
#6975=VECTOR('',#26309,10.);
#6976=VECTOR('',#26310,10.);
#6977=VECTOR('',#26311,10.);
#6978=VECTOR('',#26314,10.);
#6979=VECTOR('',#26315,10.);
#6980=VECTOR('',#26316,10.);
#6981=VECTOR('',#26319,10.);
#6982=VECTOR('',#26320,10.);
#6983=VECTOR('',#26321,10.);
#6984=VECTOR('',#26324,10.);
#6985=VECTOR('',#26325,10.);
#6986=VECTOR('',#26326,10.);
#6987=VECTOR('',#26329,10.);
#6988=VECTOR('',#26330,10.);
#6989=VECTOR('',#26339,5.);
#7567=CIRCLE('',#22992,2.942);
#7568=CIRCLE('',#23008,2.37175);
#7569=CIRCLE('',#23024,2.942);
#7570=CIRCLE('',#23025,2.);
#7571=CIRCLE('',#23027,2.37175);
#7572=CIRCLE('',#23037,5.);
#7573=CIRCLE('',#23039,5.);
#8965=VERTEX_POINT('',#70459);
#8966=VERTEX_POINT('',#70460);
#8967=VERTEX_POINT('',#70462);
#8968=VERTEX_POINT('',#70473);
#8969=VERTEX_POINT('',#70483);
#8970=VERTEX_POINT('',#70484);
#8971=VERTEX_POINT('',#70531);
#8972=VERTEX_POINT('',#70532);
#8973=VERTEX_POINT('',#70579);
#8974=VERTEX_POINT('',#70580);
#8975=VERTEX_POINT('',#70633);
#8976=VERTEX_POINT('',#70634);
#8977=VERTEX_POINT('',#70681);
#8978=VERTEX_POINT('',#70682);
#8979=VERTEX_POINT('',#70729);
#8980=VERTEX_POINT('',#70730);
#8981=VERTEX_POINT('',#70783);
#8982=VERTEX_POINT('',#70784);
#8983=VERTEX_POINT('',#70831);
#8984=VERTEX_POINT('',#70832);
#8985=VERTEX_POINT('',#70879);
#8986=VERTEX_POINT('',#70880);
#8987=VERTEX_POINT('',#70933);
#8988=VERTEX_POINT('',#70934);
#8989=VERTEX_POINT('',#70981);
#8990=VERTEX_POINT('',#70982);
#8991=VERTEX_POINT('',#71029);
#8992=VERTEX_POINT('',#71030);
#8993=VERTEX_POINT('',#71083);
#8994=VERTEX_POINT('',#71084);
#8995=VERTEX_POINT('',#71131);
#8996=VERTEX_POINT('',#71132);
#8997=VERTEX_POINT('',#71179);
#8998=VERTEX_POINT('',#71180);
#8999=VERTEX_POINT('',#71182);
#9000=VERTEX_POINT('',#71193);
#9001=VERTEX_POINT('',#71204);
#9002=VERTEX_POINT('',#71205);
#9003=VERTEX_POINT('',#71229);
#9004=VERTEX_POINT('',#71230);
#9005=VERTEX_POINT('',#71253);
#9006=VERTEX_POINT('',#71254);
#9007=VERTEX_POINT('',#71278);
#9008=VERTEX_POINT('',#71279);
#9009=VERTEX_POINT('',#71303);
#9010=VERTEX_POINT('',#71304);
#9011=VERTEX_POINT('',#71327);
#9012=VERTEX_POINT('',#71328);
#9013=VERTEX_POINT('',#71352);
#9014=VERTEX_POINT('',#71353);
#9015=VERTEX_POINT('',#71377);
#9016=VERTEX_POINT('',#71378);
#9017=VERTEX_POINT('',#71401);
#9018=VERTEX_POINT('',#71402);
#9019=VERTEX_POINT('',#71426);
#9020=VERTEX_POINT('',#71427);
#9021=VERTEX_POINT('',#71451);
#9022=VERTEX_POINT('',#71452);
#9023=VERTEX_POINT('',#71475);
#9024=VERTEX_POINT('',#71476);
#9025=VERTEX_POINT('',#71500);
#9026=VERTEX_POINT('',#71501);
#9027=VERTEX_POINT('',#71525);
#9028=VERTEX_POINT('',#71526);
#9029=VERTEX_POINT('',#71549);
#9030=VERTEX_POINT('',#71770);
#9031=VERTEX_POINT('',#71835);
#9032=VERTEX_POINT('',#71868);
#9033=VERTEX_POINT('',#72279);
#9034=VERTEX_POINT('',#72396);
#9035=VERTEX_POINT('',#72935);
#9036=VERTEX_POINT('',#72936);
#9037=VERTEX_POINT('',#72938);
#9038=VERTEX_POINT('',#72940);
#9039=VERTEX_POINT('',#72944);
#9040=VERTEX_POINT('',#72946);
#9041=VERTEX_POINT('',#72950);
#9042=VERTEX_POINT('',#72952);
#9043=VERTEX_POINT('',#72956);
#9044=VERTEX_POINT('',#72958);
#9045=VERTEX_POINT('',#72962);
#9046=VERTEX_POINT('',#72964);
#9047=VERTEX_POINT('',#72972);
#9048=VERTEX_POINT('',#72975);
#11840=EDGE_CURVE('',#8965,#8966,#5726,.T.);
#11841=EDGE_CURVE('',#8965,#8967,#1410,.T.);
#11842=EDGE_CURVE('',#8967,#8968,#7567,.F.);
#11843=EDGE_CURVE('',#8968,#8966,#1411,.T.);
#11844=EDGE_CURVE('',#8969,#8970,#5727,.T.);
#11845=EDGE_CURVE('',#8969,#8965,#1412,.T.);
#11846=EDGE_CURVE('',#8966,#8970,#1413,.T.);
#11847=EDGE_CURVE('',#8971,#8972,#5728,.T.);
#11848=EDGE_CURVE('',#8971,#8969,#1414,.T.);
#11849=EDGE_CURVE('',#8970,#8972,#1415,.T.);
#11850=EDGE_CURVE('',#8973,#8974,#5729,.T.);
#11851=EDGE_CURVE('',#8973,#8971,#1416,.T.);
#11852=EDGE_CURVE('',#8972,#8974,#1417,.T.);
#11853=EDGE_CURVE('',#8975,#8976,#5730,.T.);
#11854=EDGE_CURVE('',#8975,#8973,#1418,.T.);
#11855=EDGE_CURVE('',#8974,#8976,#1419,.T.);
#11856=EDGE_CURVE('',#8977,#8978,#5731,.T.);
#11857=EDGE_CURVE('',#8977,#8975,#1420,.T.);
#11858=EDGE_CURVE('',#8976,#8978,#1421,.T.);
#11859=EDGE_CURVE('',#8979,#8980,#5732,.T.);
#11860=EDGE_CURVE('',#8979,#8977,#1422,.T.);
#11861=EDGE_CURVE('',#8978,#8980,#1423,.T.);
#11862=EDGE_CURVE('',#8981,#8982,#5733,.T.);
#11863=EDGE_CURVE('',#8981,#8979,#1424,.T.);
#11864=EDGE_CURVE('',#8980,#8982,#1425,.T.);
#11865=EDGE_CURVE('',#8983,#8984,#5734,.T.);
#11866=EDGE_CURVE('',#8983,#8981,#1426,.T.);
#11867=EDGE_CURVE('',#8982,#8984,#1427,.T.);
#11868=EDGE_CURVE('',#8985,#8986,#5735,.T.);
#11869=EDGE_CURVE('',#8985,#8983,#1428,.T.);
#11870=EDGE_CURVE('',#8984,#8986,#1429,.T.);
#11871=EDGE_CURVE('',#8987,#8988,#5736,.T.);
#11872=EDGE_CURVE('',#8987,#8985,#1430,.T.);
#11873=EDGE_CURVE('',#8986,#8988,#1431,.T.);
#11874=EDGE_CURVE('',#8989,#8990,#5737,.T.);
#11875=EDGE_CURVE('',#8989,#8987,#1432,.T.);
#11876=EDGE_CURVE('',#8988,#8990,#1433,.T.);
#11877=EDGE_CURVE('',#8991,#8992,#5738,.T.);
#11878=EDGE_CURVE('',#8991,#8989,#1434,.T.);
#11879=EDGE_CURVE('',#8990,#8992,#1435,.T.);
#11880=EDGE_CURVE('',#8993,#8994,#5739,.T.);
#11881=EDGE_CURVE('',#8993,#8991,#1436,.T.);
#11882=EDGE_CURVE('',#8992,#8994,#1437,.T.);
#11883=EDGE_CURVE('',#8995,#8996,#5740,.T.);
#11884=EDGE_CURVE('',#8995,#8993,#1438,.T.);
#11885=EDGE_CURVE('',#8994,#8996,#1439,.T.);
#11886=EDGE_CURVE('',#8997,#8998,#5741,.T.);
#11887=EDGE_CURVE('',#8997,#8999,#1440,.T.);
#11888=EDGE_CURVE('',#8999,#9000,#7568,.T.);
#11889=EDGE_CURVE('',#8998,#9000,#1441,.T.);
#11890=EDGE_CURVE('',#9001,#9002,#5742,.T.);
#11891=EDGE_CURVE('',#9001,#8997,#1442,.T.);
#11892=EDGE_CURVE('',#9002,#8998,#1443,.T.);
#11893=EDGE_CURVE('',#9003,#9004,#5743,.T.);
#11894=EDGE_CURVE('',#9003,#9001,#1444,.T.);
#11895=EDGE_CURVE('',#9004,#9002,#1445,.T.);
#11896=EDGE_CURVE('',#9005,#9006,#5744,.T.);
#11897=EDGE_CURVE('',#9005,#9003,#1446,.T.);
#11898=EDGE_CURVE('',#9006,#9004,#1447,.T.);
#11899=EDGE_CURVE('',#9007,#9008,#5745,.T.);
#11900=EDGE_CURVE('',#9007,#9005,#1448,.T.);
#11901=EDGE_CURVE('',#9008,#9006,#1449,.T.);
#11902=EDGE_CURVE('',#9009,#9010,#5746,.T.);
#11903=EDGE_CURVE('',#9009,#9007,#1450,.T.);
#11904=EDGE_CURVE('',#9010,#9008,#1451,.T.);
#11905=EDGE_CURVE('',#9011,#9012,#5747,.T.);
#11906=EDGE_CURVE('',#9011,#9009,#1452,.T.);
#11907=EDGE_CURVE('',#9012,#9010,#1453,.T.);
#11908=EDGE_CURVE('',#9013,#9014,#5748,.T.);
#11909=EDGE_CURVE('',#9013,#9011,#1454,.T.);
#11910=EDGE_CURVE('',#9014,#9012,#1455,.T.);
#11911=EDGE_CURVE('',#9015,#9016,#5749,.T.);
#11912=EDGE_CURVE('',#9015,#9013,#1456,.T.);
#11913=EDGE_CURVE('',#9016,#9014,#1457,.T.);
#11914=EDGE_CURVE('',#9017,#9018,#5750,.T.);
#11915=EDGE_CURVE('',#9017,#9015,#1458,.T.);
#11916=EDGE_CURVE('',#9018,#9016,#1459,.T.);
#11917=EDGE_CURVE('',#9019,#9020,#5751,.T.);
#11918=EDGE_CURVE('',#9019,#9017,#1460,.T.);
#11919=EDGE_CURVE('',#9020,#9018,#1461,.T.);
#11920=EDGE_CURVE('',#9021,#9022,#5752,.T.);
#11921=EDGE_CURVE('',#9021,#9019,#1462,.T.);
#11922=EDGE_CURVE('',#9022,#9020,#1463,.T.);
#11923=EDGE_CURVE('',#9023,#9024,#5753,.T.);
#11924=EDGE_CURVE('',#9023,#9021,#1464,.T.);
#11925=EDGE_CURVE('',#9024,#9022,#1465,.T.);
#11926=EDGE_CURVE('',#9025,#9026,#5754,.T.);
#11927=EDGE_CURVE('',#9025,#9023,#1466,.T.);
#11928=EDGE_CURVE('',#9026,#9024,#1467,.T.);
#11929=EDGE_CURVE('',#9027,#9028,#5755,.T.);
#11930=EDGE_CURVE('',#9027,#9025,#1468,.T.);
#11931=EDGE_CURVE('',#9028,#9026,#1469,.T.);
#11932=EDGE_CURVE('',#9000,#9029,#1470,.T.);
#11933=EDGE_CURVE('',#9030,#8999,#1471,.T.);
#11934=EDGE_CURVE('',#9031,#9030,#7569,.T.);
#11935=EDGE_CURVE('',#9029,#9031,#1472,.T.);
#11936=EDGE_CURVE('',#9029,#9032,#5756,.T.);
#11937=EDGE_CURVE('',#9032,#9032,#7570,.T.);
#11938=EDGE_CURVE('',#9033,#9027,#1473,.T.);
#11939=EDGE_CURVE('',#8967,#9033,#1474,.T.);
#11940=EDGE_CURVE('',#9030,#8995,#1475,.T.);
#11941=EDGE_CURVE('',#9034,#9028,#1476,.T.);
#11942=EDGE_CURVE('',#9033,#9034,#7571,.T.);
#11943=EDGE_CURVE('',#8996,#9031,#1477,.T.);
#11944=EDGE_CURVE('',#9034,#8968,#1478,.T.);
#11945=EDGE_CURVE('',#9035,#9036,#5757,.T.);
#11946=EDGE_CURVE('',#9035,#9037,#5758,.T.);
#11947=EDGE_CURVE('',#9037,#9038,#5759,.T.);
#11948=EDGE_CURVE('',#9036,#9038,#5760,.T.);
#11949=EDGE_CURVE('',#9039,#9035,#5761,.T.);
#11950=EDGE_CURVE('',#9039,#9040,#5762,.T.);
#11951=EDGE_CURVE('',#9040,#9037,#5763,.T.);
#11952=EDGE_CURVE('',#9041,#9039,#5764,.T.);
#11953=EDGE_CURVE('',#9041,#9042,#5765,.T.);
#11954=EDGE_CURVE('',#9042,#9040,#5766,.T.);
#11955=EDGE_CURVE('',#9043,#9041,#5767,.T.);
#11956=EDGE_CURVE('',#9043,#9044,#5768,.T.);
#11957=EDGE_CURVE('',#9044,#9042,#5769,.T.);
#11958=EDGE_CURVE('',#9045,#9043,#5770,.T.);
#11959=EDGE_CURVE('',#9045,#9046,#5771,.T.);
#11960=EDGE_CURVE('',#9046,#9044,#5772,.T.);
#11961=EDGE_CURVE('',#9036,#9045,#5773,.T.);
#11962=EDGE_CURVE('',#9038,#9046,#5774,.T.);
#11963=EDGE_CURVE('',#9047,#9047,#7572,.T.);
#11964=EDGE_CURVE('',#9047,#9048,#5775,.T.);
#11965=EDGE_CURVE('',#9048,#9048,#7573,.T.);
#17166=ORIENTED_EDGE('',*,*,#11840,.F.);
#17167=ORIENTED_EDGE('',*,*,#11841,.T.);
#17168=ORIENTED_EDGE('',*,*,#11842,.T.);
#17169=ORIENTED_EDGE('',*,*,#11843,.T.);
#17170=ORIENTED_EDGE('',*,*,#11844,.F.);
#17171=ORIENTED_EDGE('',*,*,#11845,.T.);
#17172=ORIENTED_EDGE('',*,*,#11840,.T.);
#17173=ORIENTED_EDGE('',*,*,#11846,.T.);
#17174=ORIENTED_EDGE('',*,*,#11847,.F.);
#17175=ORIENTED_EDGE('',*,*,#11848,.T.);
#17176=ORIENTED_EDGE('',*,*,#11844,.T.);
#17177=ORIENTED_EDGE('',*,*,#11849,.T.);
#17178=ORIENTED_EDGE('',*,*,#11850,.F.);
#17179=ORIENTED_EDGE('',*,*,#11851,.T.);
#17180=ORIENTED_EDGE('',*,*,#11847,.T.);
#17181=ORIENTED_EDGE('',*,*,#11852,.T.);
#17182=ORIENTED_EDGE('',*,*,#11853,.F.);
#17183=ORIENTED_EDGE('',*,*,#11854,.T.);
#17184=ORIENTED_EDGE('',*,*,#11850,.T.);
#17185=ORIENTED_EDGE('',*,*,#11855,.T.);
#17186=ORIENTED_EDGE('',*,*,#11856,.F.);
#17187=ORIENTED_EDGE('',*,*,#11857,.T.);
#17188=ORIENTED_EDGE('',*,*,#11853,.T.);
#17189=ORIENTED_EDGE('',*,*,#11858,.T.);
#17190=ORIENTED_EDGE('',*,*,#11859,.F.);
#17191=ORIENTED_EDGE('',*,*,#11860,.T.);
#17192=ORIENTED_EDGE('',*,*,#11856,.T.);
#17193=ORIENTED_EDGE('',*,*,#11861,.T.);
#17194=ORIENTED_EDGE('',*,*,#11862,.F.);
#17195=ORIENTED_EDGE('',*,*,#11863,.T.);
#17196=ORIENTED_EDGE('',*,*,#11859,.T.);
#17197=ORIENTED_EDGE('',*,*,#11864,.T.);
#17198=ORIENTED_EDGE('',*,*,#11865,.F.);
#17199=ORIENTED_EDGE('',*,*,#11866,.T.);
#17200=ORIENTED_EDGE('',*,*,#11862,.T.);
#17201=ORIENTED_EDGE('',*,*,#11867,.T.);
#17202=ORIENTED_EDGE('',*,*,#11868,.F.);
#17203=ORIENTED_EDGE('',*,*,#11869,.T.);
#17204=ORIENTED_EDGE('',*,*,#11865,.T.);
#17205=ORIENTED_EDGE('',*,*,#11870,.T.);
#17206=ORIENTED_EDGE('',*,*,#11871,.F.);
#17207=ORIENTED_EDGE('',*,*,#11872,.T.);
#17208=ORIENTED_EDGE('',*,*,#11868,.T.);
#17209=ORIENTED_EDGE('',*,*,#11873,.T.);
#17210=ORIENTED_EDGE('',*,*,#11874,.F.);
#17211=ORIENTED_EDGE('',*,*,#11875,.T.);
#17212=ORIENTED_EDGE('',*,*,#11871,.T.);
#17213=ORIENTED_EDGE('',*,*,#11876,.T.);
#17214=ORIENTED_EDGE('',*,*,#11877,.F.);
#17215=ORIENTED_EDGE('',*,*,#11878,.T.);
#17216=ORIENTED_EDGE('',*,*,#11874,.T.);
#17217=ORIENTED_EDGE('',*,*,#11879,.T.);
#17218=ORIENTED_EDGE('',*,*,#11880,.F.);
#17219=ORIENTED_EDGE('',*,*,#11881,.T.);
#17220=ORIENTED_EDGE('',*,*,#11877,.T.);
#17221=ORIENTED_EDGE('',*,*,#11882,.T.);
#17222=ORIENTED_EDGE('',*,*,#11883,.F.);
#17223=ORIENTED_EDGE('',*,*,#11884,.T.);
#17224=ORIENTED_EDGE('',*,*,#11880,.T.);
#17225=ORIENTED_EDGE('',*,*,#11885,.T.);
#17226=ORIENTED_EDGE('',*,*,#11886,.F.);
#17227=ORIENTED_EDGE('',*,*,#11887,.T.);
#17228=ORIENTED_EDGE('',*,*,#11888,.T.);
#17229=ORIENTED_EDGE('',*,*,#11889,.F.);
#17230=ORIENTED_EDGE('',*,*,#11890,.F.);
#17231=ORIENTED_EDGE('',*,*,#11891,.T.);
#17232=ORIENTED_EDGE('',*,*,#11886,.T.);
#17233=ORIENTED_EDGE('',*,*,#11892,.F.);
#17234=ORIENTED_EDGE('',*,*,#11893,.F.);
#17235=ORIENTED_EDGE('',*,*,#11894,.T.);
#17236=ORIENTED_EDGE('',*,*,#11890,.T.);
#17237=ORIENTED_EDGE('',*,*,#11895,.F.);
#17238=ORIENTED_EDGE('',*,*,#11896,.F.);
#17239=ORIENTED_EDGE('',*,*,#11897,.T.);
#17240=ORIENTED_EDGE('',*,*,#11893,.T.);
#17241=ORIENTED_EDGE('',*,*,#11898,.F.);
#17242=ORIENTED_EDGE('',*,*,#11899,.F.);
#17243=ORIENTED_EDGE('',*,*,#11900,.T.);
#17244=ORIENTED_EDGE('',*,*,#11896,.T.);
#17245=ORIENTED_EDGE('',*,*,#11901,.F.);
#17246=ORIENTED_EDGE('',*,*,#11902,.F.);
#17247=ORIENTED_EDGE('',*,*,#11903,.T.);
#17248=ORIENTED_EDGE('',*,*,#11899,.T.);
#17249=ORIENTED_EDGE('',*,*,#11904,.F.);
#17250=ORIENTED_EDGE('',*,*,#11905,.F.);
#17251=ORIENTED_EDGE('',*,*,#11906,.T.);
#17252=ORIENTED_EDGE('',*,*,#11902,.T.);
#17253=ORIENTED_EDGE('',*,*,#11907,.F.);
#17254=ORIENTED_EDGE('',*,*,#11908,.F.);
#17255=ORIENTED_EDGE('',*,*,#11909,.T.);
#17256=ORIENTED_EDGE('',*,*,#11905,.T.);
#17257=ORIENTED_EDGE('',*,*,#11910,.F.);
#17258=ORIENTED_EDGE('',*,*,#11911,.F.);
#17259=ORIENTED_EDGE('',*,*,#11912,.T.);
#17260=ORIENTED_EDGE('',*,*,#11908,.T.);
#17261=ORIENTED_EDGE('',*,*,#11913,.F.);
#17262=ORIENTED_EDGE('',*,*,#11914,.F.);
#17263=ORIENTED_EDGE('',*,*,#11915,.T.);
#17264=ORIENTED_EDGE('',*,*,#11911,.T.);
#17265=ORIENTED_EDGE('',*,*,#11916,.F.);
#17266=ORIENTED_EDGE('',*,*,#11917,.F.);
#17267=ORIENTED_EDGE('',*,*,#11918,.T.);
#17268=ORIENTED_EDGE('',*,*,#11914,.T.);
#17269=ORIENTED_EDGE('',*,*,#11919,.F.);
#17270=ORIENTED_EDGE('',*,*,#11920,.F.);
#17271=ORIENTED_EDGE('',*,*,#11921,.T.);
#17272=ORIENTED_EDGE('',*,*,#11917,.T.);
#17273=ORIENTED_EDGE('',*,*,#11922,.F.);
#17274=ORIENTED_EDGE('',*,*,#11923,.F.);
#17275=ORIENTED_EDGE('',*,*,#11924,.T.);
#17276=ORIENTED_EDGE('',*,*,#11920,.T.);
#17277=ORIENTED_EDGE('',*,*,#11925,.F.);
#17278=ORIENTED_EDGE('',*,*,#11926,.F.);
#17279=ORIENTED_EDGE('',*,*,#11927,.T.);
#17280=ORIENTED_EDGE('',*,*,#11923,.T.);
#17281=ORIENTED_EDGE('',*,*,#11928,.F.);
#17282=ORIENTED_EDGE('',*,*,#11929,.F.);
#17283=ORIENTED_EDGE('',*,*,#11930,.T.);
#17284=ORIENTED_EDGE('',*,*,#11926,.T.);
#17285=ORIENTED_EDGE('',*,*,#11931,.F.);
#17286=ORIENTED_EDGE('',*,*,#11932,.F.);
#17287=ORIENTED_EDGE('',*,*,#11888,.F.);
#17288=ORIENTED_EDGE('',*,*,#11933,.F.);
#17289=ORIENTED_EDGE('',*,*,#11934,.F.);
#17290=ORIENTED_EDGE('',*,*,#11935,.F.);
#17291=ORIENTED_EDGE('',*,*,#11936,.T.);
#17292=ORIENTED_EDGE('',*,*,#11937,.F.);
#17293=ORIENTED_EDGE('',*,*,#11936,.F.);
#17294=ORIENTED_EDGE('',*,*,#11933,.T.);
#17295=ORIENTED_EDGE('',*,*,#11887,.F.);
#17296=ORIENTED_EDGE('',*,*,#11891,.F.);
#17297=ORIENTED_EDGE('',*,*,#11894,.F.);
#17298=ORIENTED_EDGE('',*,*,#11897,.F.);
#17299=ORIENTED_EDGE('',*,*,#11900,.F.);
#17300=ORIENTED_EDGE('',*,*,#11903,.F.);
#17301=ORIENTED_EDGE('',*,*,#11906,.F.);
#17302=ORIENTED_EDGE('',*,*,#11909,.F.);
#17303=ORIENTED_EDGE('',*,*,#11912,.F.);
#17304=ORIENTED_EDGE('',*,*,#11915,.F.);
#17305=ORIENTED_EDGE('',*,*,#11918,.F.);
#17306=ORIENTED_EDGE('',*,*,#11921,.F.);
#17307=ORIENTED_EDGE('',*,*,#11924,.F.);
#17308=ORIENTED_EDGE('',*,*,#11927,.F.);
#17309=ORIENTED_EDGE('',*,*,#11930,.F.);
#17310=ORIENTED_EDGE('',*,*,#11938,.F.);
#17311=ORIENTED_EDGE('',*,*,#11939,.F.);
#17312=ORIENTED_EDGE('',*,*,#11841,.F.);
#17313=ORIENTED_EDGE('',*,*,#11845,.F.);
#17314=ORIENTED_EDGE('',*,*,#11848,.F.);
#17315=ORIENTED_EDGE('',*,*,#11851,.F.);
#17316=ORIENTED_EDGE('',*,*,#11854,.F.);
#17317=ORIENTED_EDGE('',*,*,#11857,.F.);
#17318=ORIENTED_EDGE('',*,*,#11860,.F.);
#17319=ORIENTED_EDGE('',*,*,#11863,.F.);
#17320=ORIENTED_EDGE('',*,*,#11866,.F.);
#17321=ORIENTED_EDGE('',*,*,#11869,.F.);
#17322=ORIENTED_EDGE('',*,*,#11872,.F.);
#17323=ORIENTED_EDGE('',*,*,#11875,.F.);
#17324=ORIENTED_EDGE('',*,*,#11878,.F.);
#17325=ORIENTED_EDGE('',*,*,#11881,.F.);
#17326=ORIENTED_EDGE('',*,*,#11884,.F.);
#17327=ORIENTED_EDGE('',*,*,#11940,.F.);
#17328=ORIENTED_EDGE('',*,*,#11929,.T.);
#17329=ORIENTED_EDGE('',*,*,#11941,.F.);
#17330=ORIENTED_EDGE('',*,*,#11942,.F.);
#17331=ORIENTED_EDGE('',*,*,#11938,.T.);
#17332=ORIENTED_EDGE('',*,*,#11932,.T.);
#17333=ORIENTED_EDGE('',*,*,#11935,.T.);
#17334=ORIENTED_EDGE('',*,*,#11943,.F.);
#17335=ORIENTED_EDGE('',*,*,#11885,.F.);
#17336=ORIENTED_EDGE('',*,*,#11882,.F.);
#17337=ORIENTED_EDGE('',*,*,#11879,.F.);
#17338=ORIENTED_EDGE('',*,*,#11876,.F.);
#17339=ORIENTED_EDGE('',*,*,#11873,.F.);
#17340=ORIENTED_EDGE('',*,*,#11870,.F.);
#17341=ORIENTED_EDGE('',*,*,#11867,.F.);
#17342=ORIENTED_EDGE('',*,*,#11864,.F.);
#17343=ORIENTED_EDGE('',*,*,#11861,.F.);
#17344=ORIENTED_EDGE('',*,*,#11858,.F.);
#17345=ORIENTED_EDGE('',*,*,#11855,.F.);
#17346=ORIENTED_EDGE('',*,*,#11852,.F.);
#17347=ORIENTED_EDGE('',*,*,#11849,.F.);
#17348=ORIENTED_EDGE('',*,*,#11846,.F.);
#17349=ORIENTED_EDGE('',*,*,#11843,.F.);
#17350=ORIENTED_EDGE('',*,*,#11944,.F.);
#17351=ORIENTED_EDGE('',*,*,#11941,.T.);
#17352=ORIENTED_EDGE('',*,*,#11931,.T.);
#17353=ORIENTED_EDGE('',*,*,#11928,.T.);
#17354=ORIENTED_EDGE('',*,*,#11925,.T.);
#17355=ORIENTED_EDGE('',*,*,#11922,.T.);
#17356=ORIENTED_EDGE('',*,*,#11919,.T.);
#17357=ORIENTED_EDGE('',*,*,#11916,.T.);
#17358=ORIENTED_EDGE('',*,*,#11913,.T.);
#17359=ORIENTED_EDGE('',*,*,#11910,.T.);
#17360=ORIENTED_EDGE('',*,*,#11907,.T.);
#17361=ORIENTED_EDGE('',*,*,#11904,.T.);
#17362=ORIENTED_EDGE('',*,*,#11901,.T.);
#17363=ORIENTED_EDGE('',*,*,#11898,.T.);
#17364=ORIENTED_EDGE('',*,*,#11895,.T.);
#17365=ORIENTED_EDGE('',*,*,#11892,.T.);
#17366=ORIENTED_EDGE('',*,*,#11889,.T.);
#17367=ORIENTED_EDGE('',*,*,#11883,.T.);
#17368=ORIENTED_EDGE('',*,*,#11943,.T.);
#17369=ORIENTED_EDGE('',*,*,#11934,.T.);
#17370=ORIENTED_EDGE('',*,*,#11940,.T.);
#17371=ORIENTED_EDGE('',*,*,#11945,.F.);
#17372=ORIENTED_EDGE('',*,*,#11946,.T.);
#17373=ORIENTED_EDGE('',*,*,#11947,.T.);
#17374=ORIENTED_EDGE('',*,*,#11948,.F.);
#17375=ORIENTED_EDGE('',*,*,#11949,.F.);
#17376=ORIENTED_EDGE('',*,*,#11950,.T.);
#17377=ORIENTED_EDGE('',*,*,#11951,.T.);
#17378=ORIENTED_EDGE('',*,*,#11946,.F.);
#17379=ORIENTED_EDGE('',*,*,#11952,.F.);
#17380=ORIENTED_EDGE('',*,*,#11953,.T.);
#17381=ORIENTED_EDGE('',*,*,#11954,.T.);
#17382=ORIENTED_EDGE('',*,*,#11950,.F.);
#17383=ORIENTED_EDGE('',*,*,#11955,.F.);
#17384=ORIENTED_EDGE('',*,*,#11956,.T.);
#17385=ORIENTED_EDGE('',*,*,#11957,.T.);
#17386=ORIENTED_EDGE('',*,*,#11953,.F.);
#17387=ORIENTED_EDGE('',*,*,#11958,.F.);
#17388=ORIENTED_EDGE('',*,*,#11959,.T.);
#17389=ORIENTED_EDGE('',*,*,#11960,.T.);
#17390=ORIENTED_EDGE('',*,*,#11956,.F.);
#17391=ORIENTED_EDGE('',*,*,#11961,.F.);
#17392=ORIENTED_EDGE('',*,*,#11948,.T.);
#17393=ORIENTED_EDGE('',*,*,#11962,.T.);
#17394=ORIENTED_EDGE('',*,*,#11959,.F.);
#17395=ORIENTED_EDGE('',*,*,#11962,.F.);
#17396=ORIENTED_EDGE('',*,*,#11947,.F.);
#17397=ORIENTED_EDGE('',*,*,#11951,.F.);
#17398=ORIENTED_EDGE('',*,*,#11954,.F.);
#17399=ORIENTED_EDGE('',*,*,#11957,.F.);
#17400=ORIENTED_EDGE('',*,*,#11960,.F.);
#17401=ORIENTED_EDGE('',*,*,#11963,.T.);
#17402=ORIENTED_EDGE('',*,*,#11939,.T.);
#17403=ORIENTED_EDGE('',*,*,#11942,.T.);
#17404=ORIENTED_EDGE('',*,*,#11944,.T.);
#17405=ORIENTED_EDGE('',*,*,#11842,.F.);
#17406=ORIENTED_EDGE('',*,*,#11963,.F.);
#17407=ORIENTED_EDGE('',*,*,#11964,.T.);
#17408=ORIENTED_EDGE('',*,*,#11965,.T.);
#17409=ORIENTED_EDGE('',*,*,#11964,.F.);
#17410=ORIENTED_EDGE('',*,*,#11965,.F.);
#17411=ORIENTED_EDGE('',*,*,#11945,.T.);
#17412=ORIENTED_EDGE('',*,*,#11961,.T.);
#17413=ORIENTED_EDGE('',*,*,#11958,.T.);
#17414=ORIENTED_EDGE('',*,*,#11955,.T.);
#17415=ORIENTED_EDGE('',*,*,#11952,.T.);
#17416=ORIENTED_EDGE('',*,*,#11949,.T.);
#17417=ORIENTED_EDGE('',*,*,#11937,.T.);
#20267=CYLINDRICAL_SURFACE('',#22991,2.942);
#20268=CYLINDRICAL_SURFACE('',#22993,2.942);
#20269=CYLINDRICAL_SURFACE('',#22994,2.942);
#20270=CYLINDRICAL_SURFACE('',#22995,2.942);
#20271=CYLINDRICAL_SURFACE('',#22996,2.942);
#20272=CYLINDRICAL_SURFACE('',#22997,2.942);
#20273=CYLINDRICAL_SURFACE('',#22998,2.942);
#20274=CYLINDRICAL_SURFACE('',#22999,2.942);
#20275=CYLINDRICAL_SURFACE('',#23000,2.942);
#20276=CYLINDRICAL_SURFACE('',#23001,2.942);
#20277=CYLINDRICAL_SURFACE('',#23002,2.942);
#20278=CYLINDRICAL_SURFACE('',#23003,2.942);
#20279=CYLINDRICAL_SURFACE('',#23004,2.942);
#20280=CYLINDRICAL_SURFACE('',#23005,2.942);
#20281=CYLINDRICAL_SURFACE('',#23006,2.942);
#20282=CYLINDRICAL_SURFACE('',#23007,2.37175);
#20283=CYLINDRICAL_SURFACE('',#23009,2.37175);
#20284=CYLINDRICAL_SURFACE('',#23010,2.37175);
#20285=CYLINDRICAL_SURFACE('',#23011,2.37175);
#20286=CYLINDRICAL_SURFACE('',#23012,2.37175);
#20287=CYLINDRICAL_SURFACE('',#23013,2.37175);
#20288=CYLINDRICAL_SURFACE('',#23014,2.37175);
#20289=CYLINDRICAL_SURFACE('',#23015,2.37175);
#20290=CYLINDRICAL_SURFACE('',#23016,2.37175);
#20291=CYLINDRICAL_SURFACE('',#23017,2.37175);
#20292=CYLINDRICAL_SURFACE('',#23018,2.37175);
#20293=CYLINDRICAL_SURFACE('',#23019,2.37175);
#20294=CYLINDRICAL_SURFACE('',#23020,2.37175);
#20295=CYLINDRICAL_SURFACE('',#23021,2.37175);
#20296=CYLINDRICAL_SURFACE('',#23022,2.37175);
#20297=CYLINDRICAL_SURFACE('',#23026,2.37175);
#20298=CYLINDRICAL_SURFACE('',#23028,2.942);
#20299=CYLINDRICAL_SURFACE('',#23038,5.);
#21373=ADVANCED_FACE('',(#3253),#20267,.T.);
#21374=ADVANCED_FACE('',(#3254),#20268,.T.);
#21375=ADVANCED_FACE('',(#3255),#20269,.T.);
#21376=ADVANCED_FACE('',(#3256),#20270,.T.);
#21377=ADVANCED_FACE('',(#3257),#20271,.T.);
#21378=ADVANCED_FACE('',(#3258),#20272,.T.);
#21379=ADVANCED_FACE('',(#3259),#20273,.T.);
#21380=ADVANCED_FACE('',(#3260),#20274,.T.);
#21381=ADVANCED_FACE('',(#3261),#20275,.T.);
#21382=ADVANCED_FACE('',(#3262),#20276,.T.);
#21383=ADVANCED_FACE('',(#3263),#20277,.T.);
#21384=ADVANCED_FACE('',(#3264),#20278,.T.);
#21385=ADVANCED_FACE('',(#3265),#20279,.T.);
#21386=ADVANCED_FACE('',(#3266),#20280,.T.);
#21387=ADVANCED_FACE('',(#3267),#20281,.T.);
#21388=ADVANCED_FACE('',(#3268),#20282,.T.);
#21389=ADVANCED_FACE('',(#3269),#20283,.T.);
#21390=ADVANCED_FACE('',(#3270),#20284,.T.);
#21391=ADVANCED_FACE('',(#3271),#20285,.T.);
#21392=ADVANCED_FACE('',(#3272),#20286,.T.);
#21393=ADVANCED_FACE('',(#3273),#20287,.T.);
#21394=ADVANCED_FACE('',(#3274),#20288,.T.);
#21395=ADVANCED_FACE('',(#3275),#20289,.T.);
#21396=ADVANCED_FACE('',(#3276),#20290,.T.);
#21397=ADVANCED_FACE('',(#3277),#20291,.T.);
#21398=ADVANCED_FACE('',(#3278),#20292,.T.);
#21399=ADVANCED_FACE('',(#3279),#20293,.T.);
#21400=ADVANCED_FACE('',(#3280),#20294,.T.);
#21401=ADVANCED_FACE('',(#3281),#20295,.T.);
#21402=ADVANCED_FACE('',(#3282),#20296,.T.);
#21403=ADVANCED_FACE('',(#3283),#332,.T.);
#21404=ADVANCED_FACE('',(#3284),#360,.F.);
#21405=ADVANCED_FACE('',(#3285),#20297,.T.);
#21406=ADVANCED_FACE('',(#3286),#361,.F.);
#21407=ADVANCED_FACE('',(#3287),#20298,.T.);
#21408=ADVANCED_FACE('',(#3288),#2507,.F.);
#21409=ADVANCED_FACE('',(#3289),#2508,.F.);
#21410=ADVANCED_FACE('',(#3290),#2509,.F.);
#21411=ADVANCED_FACE('',(#3291),#2510,.F.);
#21412=ADVANCED_FACE('',(#3292),#2511,.F.);
#21413=ADVANCED_FACE('',(#3293),#2512,.F.);
#21414=ADVANCED_FACE('',(#3294),#2513,.F.);
#21415=ADVANCED_FACE('',(#3295,#2359),#2514,.T.);
#21416=ADVANCED_FACE('',(#3296),#20299,.T.);
#21417=ADVANCED_FACE('',(#3297,#2360),#2515,.F.);
#21418=ADVANCED_FACE('',(#3298),#2516,.T.);
#21825=CLOSED_SHELL('',(#21373,#21374,#21375,#21376,#21377,#21378,#21379,
#21380,#21381,#21382,#21383,#21384,#21385,#21386,#21387,#21388,#21389,#21390,
#21391,#21392,#21393,#21394,#21395,#21396,#21397,#21398,#21399,#21400,#21401,
#21402,#21403,#21404,#21405,#21406,#21407,#21408,#21409,#21410,#21411,#21412,
#21413,#21414,#21415,#21416,#21417,#21418));
#22990=AXIS2_PLACEMENT_3D('',#70457,#26192,#26193);
#22991=AXIS2_PLACEMENT_3D('',#70458,#26194,#26195);
#22992=AXIS2_PLACEMENT_3D('',#70474,#26197,#26198);
#22993=AXIS2_PLACEMENT_3D('',#70482,#26199,#26200);
#22994=AXIS2_PLACEMENT_3D('',#70530,#26202,#26203);
#22995=AXIS2_PLACEMENT_3D('',#70578,#26205,#26206);
#22996=AXIS2_PLACEMENT_3D('',#70632,#26208,#26209);
#22997=AXIS2_PLACEMENT_3D('',#70680,#26211,#26212);
#22998=AXIS2_PLACEMENT_3D('',#70728,#26214,#26215);
#22999=AXIS2_PLACEMENT_3D('',#70782,#26217,#26218);
#23000=AXIS2_PLACEMENT_3D('',#70830,#26220,#26221);
#23001=AXIS2_PLACEMENT_3D('',#70878,#26223,#26224);
#23002=AXIS2_PLACEMENT_3D('',#70932,#26226,#26227);
#23003=AXIS2_PLACEMENT_3D('',#70980,#26229,#26230);
#23004=AXIS2_PLACEMENT_3D('',#71028,#26232,#26233);
#23005=AXIS2_PLACEMENT_3D('',#71082,#26235,#26236);
#23006=AXIS2_PLACEMENT_3D('',#71130,#26238,#26239);
#23007=AXIS2_PLACEMENT_3D('',#71178,#26241,#26242);
#23008=AXIS2_PLACEMENT_3D('',#71194,#26244,#26245);
#23009=AXIS2_PLACEMENT_3D('',#71203,#26246,#26247);
#23010=AXIS2_PLACEMENT_3D('',#71228,#26249,#26250);
#23011=AXIS2_PLACEMENT_3D('',#71252,#26252,#26253);
#23012=AXIS2_PLACEMENT_3D('',#71277,#26255,#26256);
#23013=AXIS2_PLACEMENT_3D('',#71302,#26258,#26259);
#23014=AXIS2_PLACEMENT_3D('',#71326,#26261,#26262);
#23015=AXIS2_PLACEMENT_3D('',#71351,#26264,#26265);
#23016=AXIS2_PLACEMENT_3D('',#71376,#26267,#26268);
#23017=AXIS2_PLACEMENT_3D('',#71400,#26270,#26271);
#23018=AXIS2_PLACEMENT_3D('',#71425,#26273,#26274);
#23019=AXIS2_PLACEMENT_3D('',#71450,#26276,#26277);
#23020=AXIS2_PLACEMENT_3D('',#71474,#26279,#26280);
#23021=AXIS2_PLACEMENT_3D('',#71499,#26282,#26283);
#23022=AXIS2_PLACEMENT_3D('',#71524,#26285,#26286);
#23023=AXIS2_PLACEMENT_3D('',#71548,#26288,#26289);
#23024=AXIS2_PLACEMENT_3D('',#71836,#26290,#26291);
#23025=AXIS2_PLACEMENT_3D('',#71870,#26293,#26294);
#23026=AXIS2_PLACEMENT_3D('',#72395,#26295,#26296);
#23027=AXIS2_PLACEMENT_3D('',#72406,#26297,#26298);
#23028=AXIS2_PLACEMENT_3D('',#72933,#26299,#26300);
#23029=AXIS2_PLACEMENT_3D('',#72934,#26301,#26302);
#23030=AXIS2_PLACEMENT_3D('',#72943,#26307,#26308);
#23031=AXIS2_PLACEMENT_3D('',#72949,#26312,#26313);
#23032=AXIS2_PLACEMENT_3D('',#72955,#26317,#26318);
#23033=AXIS2_PLACEMENT_3D('',#72961,#26322,#26323);
#23034=AXIS2_PLACEMENT_3D('',#72967,#26327,#26328);
#23035=AXIS2_PLACEMENT_3D('',#72970,#26331,#26332);
#23036=AXIS2_PLACEMENT_3D('',#72971,#26333,#26334);
#23037=AXIS2_PLACEMENT_3D('',#72973,#26335,#26336);
#23038=AXIS2_PLACEMENT_3D('',#72974,#26337,#26338);
#23039=AXIS2_PLACEMENT_3D('',#72977,#26340,#26341);
#23040=AXIS2_PLACEMENT_3D('',#72978,#26342,#26343);
#23041=AXIS2_PLACEMENT_3D('',#72979,#26344,#26345);
#26192=DIRECTION('axis',(0.,0.,1.));
#26193=DIRECTION('refdir',(1.,0.,0.));
#26194=DIRECTION('center_axis',(0.,0.,1.));
#26195=DIRECTION('ref_axis',(1.,0.,0.));
#26196=DIRECTION('',(0.,0.,-1.));
#26197=DIRECTION('center_axis',(0.,0.,-1.));
#26198=DIRECTION('ref_axis',(1.,0.,0.));
#26199=DIRECTION('center_axis',(0.,0.,1.));
#26200=DIRECTION('ref_axis',(1.,0.,0.));
#26201=DIRECTION('',(0.,0.,-1.));
#26202=DIRECTION('center_axis',(0.,0.,1.));
#26203=DIRECTION('ref_axis',(1.,0.,0.));
#26204=DIRECTION('',(0.,0.,-1.));
#26205=DIRECTION('center_axis',(0.,0.,1.));
#26206=DIRECTION('ref_axis',(1.,0.,0.));
#26207=DIRECTION('',(0.,0.,-1.));
#26208=DIRECTION('center_axis',(0.,0.,1.));
#26209=DIRECTION('ref_axis',(1.,0.,0.));
#26210=DIRECTION('',(0.,0.,-1.));
#26211=DIRECTION('center_axis',(0.,0.,1.));
#26212=DIRECTION('ref_axis',(1.,0.,0.));
#26213=DIRECTION('',(0.,0.,-1.));
#26214=DIRECTION('center_axis',(0.,0.,1.));
#26215=DIRECTION('ref_axis',(1.,0.,0.));
#26216=DIRECTION('',(0.,0.,-1.));
#26217=DIRECTION('center_axis',(0.,0.,1.));
#26218=DIRECTION('ref_axis',(1.,0.,0.));
#26219=DIRECTION('',(0.,0.,-1.));
#26220=DIRECTION('center_axis',(0.,0.,1.));
#26221=DIRECTION('ref_axis',(1.,0.,0.));
#26222=DIRECTION('',(0.,0.,-1.));
#26223=DIRECTION('center_axis',(0.,0.,1.));
#26224=DIRECTION('ref_axis',(1.,0.,0.));
#26225=DIRECTION('',(0.,0.,-1.));
#26226=DIRECTION('center_axis',(0.,0.,1.));
#26227=DIRECTION('ref_axis',(1.,0.,0.));
#26228=DIRECTION('',(0.,0.,-1.));
#26229=DIRECTION('center_axis',(0.,0.,1.));
#26230=DIRECTION('ref_axis',(1.,0.,0.));
#26231=DIRECTION('',(0.,0.,-1.));
#26232=DIRECTION('center_axis',(0.,0.,1.));
#26233=DIRECTION('ref_axis',(1.,0.,0.));
#26234=DIRECTION('',(0.,0.,-1.));
#26235=DIRECTION('center_axis',(0.,0.,1.));
#26236=DIRECTION('ref_axis',(1.,0.,0.));
#26237=DIRECTION('',(0.,0.,-1.));
#26238=DIRECTION('center_axis',(0.,0.,1.));
#26239=DIRECTION('ref_axis',(1.,0.,0.));
#26240=DIRECTION('',(0.,0.,-1.));
#26241=DIRECTION('center_axis',(0.,0.,1.));
#26242=DIRECTION('ref_axis',(0.997339946684471,-0.0728905394918792,0.));
#26243=DIRECTION('',(0.,0.,1.));
#26244=DIRECTION('center_axis',(0.,0.,-1.));
#26245=DIRECTION('ref_axis',(1.,1.10476514494527E-13,0.));
#26246=DIRECTION('center_axis',(0.,0.,1.));
#26247=DIRECTION('ref_axis',(1.,1.10476514494527E-13,0.));
#26248=DIRECTION('',(0.,0.,1.));
#26249=DIRECTION('center_axis',(0.,0.,1.));
#26250=DIRECTION('ref_axis',(1.,1.10476514494527E-13,0.));
#26251=DIRECTION('',(0.,0.,1.));
#26252=DIRECTION('center_axis',(0.,0.,1.));
#26253=DIRECTION('ref_axis',(1.,1.10476514494527E-13,0.));
#26254=DIRECTION('',(0.,0.,1.));
#26255=DIRECTION('center_axis',(0.,0.,1.));
#26256=DIRECTION('ref_axis',(1.,1.10476514494527E-13,0.));
#26257=DIRECTION('',(0.,0.,1.));
#26258=DIRECTION('center_axis',(0.,0.,1.));
#26259=DIRECTION('ref_axis',(1.,1.10476514494527E-13,0.));
#26260=DIRECTION('',(0.,0.,1.));
#26261=DIRECTION('center_axis',(0.,0.,1.));
#26262=DIRECTION('ref_axis',(1.,1.10476514494527E-13,0.));
#26263=DIRECTION('',(0.,0.,1.));
#26264=DIRECTION('center_axis',(0.,0.,1.));
#26265=DIRECTION('ref_axis',(1.,1.10476514494527E-13,0.));
#26266=DIRECTION('',(0.,0.,1.));
#26267=DIRECTION('center_axis',(0.,0.,1.));
#26268=DIRECTION('ref_axis',(1.,1.10476514494527E-13,0.));
#26269=DIRECTION('',(0.,0.,1.));
#26270=DIRECTION('center_axis',(0.,0.,1.));
#26271=DIRECTION('ref_axis',(1.,1.10476514494527E-13,0.));
#26272=DIRECTION('',(0.,0.,1.));
#26273=DIRECTION('center_axis',(0.,0.,1.));
#26274=DIRECTION('ref_axis',(1.,1.10476514494527E-13,0.));
#26275=DIRECTION('',(0.,0.,1.));
#26276=DIRECTION('center_axis',(0.,0.,1.));
#26277=DIRECTION('ref_axis',(1.,1.10476514494527E-13,0.));
#26278=DIRECTION('',(0.,0.,1.));
#26279=DIRECTION('center_axis',(0.,0.,1.));
#26280=DIRECTION('ref_axis',(1.,1.10476514494527E-13,0.));
#26281=DIRECTION('',(0.,0.,1.));
#26282=DIRECTION('center_axis',(0.,0.,1.));
#26283=DIRECTION('ref_axis',(1.,1.10476514494527E-13,0.));
#26284=DIRECTION('',(0.,0.,1.));
#26285=DIRECTION('center_axis',(0.,0.,1.));
#26286=DIRECTION('ref_axis',(1.,1.10476514494527E-13,0.));
#26287=DIRECTION('',(0.,0.,1.));
#26288=DIRECTION('center_axis',(0.,0.,-1.));
#26289=DIRECTION('ref_axis',(1.,0.,0.));
#26290=DIRECTION('center_axis',(0.,0.,-1.));
#26291=DIRECTION('ref_axis',(1.,0.,0.));
#26292=DIRECTION('',(0.707106781186547,8.65956056235493E-17,0.707106781186548));
#26293=DIRECTION('center_axis',(0.,0.,1.));
#26294=DIRECTION('ref_axis',(1.,0.,0.));
#26295=DIRECTION('center_axis',(0.,0.,1.));
#26296=DIRECTION('ref_axis',(1.,1.10476514494527E-13,0.));
#26297=DIRECTION('center_axis',(0.,0.,-1.));
#26298=DIRECTION('ref_axis',(1.,1.10476514494527E-13,0.));
#26299=DIRECTION('center_axis',(0.,0.,1.));
#26300=DIRECTION('ref_axis',(1.,0.,0.));
#26301=DIRECTION('center_axis',(-1.92296268638356E-16,-1.,0.));
#26302=DIRECTION('ref_axis',(1.,-1.92296268638356E-16,0.));
#26303=DIRECTION('',(1.,-1.92296268638356E-16,0.));
#26304=DIRECTION('',(0.,0.,1.));
#26305=DIRECTION('',(1.,-1.92296268638356E-16,0.));
#26306=DIRECTION('',(0.,0.,1.));
#26307=DIRECTION('center_axis',(-0.866025403784439,-0.5,0.));
#26308=DIRECTION('ref_axis',(0.5,-0.866025403784439,0.));
#26309=DIRECTION('',(0.5,-0.866025403784439,0.));
#26310=DIRECTION('',(0.,0.,1.));
#26311=DIRECTION('',(0.5,-0.866025403784439,0.));
#26312=DIRECTION('center_axis',(-0.866025403784439,0.5,0.));
#26313=DIRECTION('ref_axis',(-0.5,-0.866025403784438,0.));
#26314=DIRECTION('',(-0.5,-0.866025403784438,0.));
#26315=DIRECTION('',(0.,0.,1.));
#26316=DIRECTION('',(-0.5,-0.866025403784439,0.));
#26317=DIRECTION('center_axis',(1.92296268638356E-16,1.,0.));
#26318=DIRECTION('ref_axis',(-1.,1.92296268638356E-16,0.));
#26319=DIRECTION('',(-1.,1.92296268638356E-16,0.));
#26320=DIRECTION('',(0.,0.,1.));
#26321=DIRECTION('',(-1.,1.92296268638356E-16,0.));
#26322=DIRECTION('center_axis',(0.866025403784439,0.5,0.));
#26323=DIRECTION('ref_axis',(-0.5,0.866025403784439,0.));
#26324=DIRECTION('',(-0.5,0.866025403784439,0.));
#26325=DIRECTION('',(0.,0.,1.));
#26326=DIRECTION('',(-0.5,0.866025403784439,0.));
#26327=DIRECTION('center_axis',(0.866025403784439,-0.5,0.));
#26328=DIRECTION('ref_axis',(0.5,0.866025403784439,0.));
#26329=DIRECTION('',(0.5,0.866025403784439,0.));
#26330=DIRECTION('',(0.5,0.866025403784439,0.));
#26331=DIRECTION('center_axis',(0.,0.,1.));
#26332=DIRECTION('ref_axis',(1.,0.,0.));
#26333=DIRECTION('center_axis',(0.,0.,1.));
#26334=DIRECTION('ref_axis',(1.,0.,0.));
#26335=DIRECTION('center_axis',(0.,0.,1.));
#26336=DIRECTION('ref_axis',(1.,0.,0.));
#26337=DIRECTION('center_axis',(0.,0.,1.));
#26338=DIRECTION('ref_axis',(1.,0.,0.));
#26339=DIRECTION('',(0.,0.,-1.));
#26340=DIRECTION('center_axis',(0.,0.,1.));
#26341=DIRECTION('ref_axis',(1.,0.,0.));
#26342=DIRECTION('center_axis',(0.,0.,1.));
#26343=DIRECTION('ref_axis',(1.,0.,0.));
#26344=DIRECTION('center_axis',(0.,0.,1.));
#26345=DIRECTION('ref_axis',(1.,0.,0.));
#70457=CARTESIAN_POINT('',(0.,0.,0.));
#70458=CARTESIAN_POINT('Origin',(0.,0.,0.));
#70459=CARTESIAN_POINT('',(-2.94490570994055,0.00214417779480537,0.322176117089595));
#70460=CARTESIAN_POINT('',(-2.94453111094736,0.00313617179185542,0.177823882910391));
#70461=CARTESIAN_POINT('',(-2.942,-3.60291088309151E-16,0.));
#70462=CARTESIAN_POINT('',(1.28892185405323,2.64462557919718,0.));
#70463=CARTESIAN_POINT('Ctrl Pts',(-2.94490570994055,0.00214417779480537,
0.322176117089595));
#70464=CARTESIAN_POINT('Ctrl Pts',(-2.94584715833611,0.124808428590093,
0.315520895872749));
#70465=CARTESIAN_POINT('Ctrl Pts',(-2.93884007386573,0.247358426874668,
0.308865674655903));
#70466=CARTESIAN_POINT('Ctrl Pts',(-2.92351947045398,0.368852411761562,
0.302210453439057));
#70467=CARTESIAN_POINT('Ctrl Pts',(-2.80238513102988,1.32946037267173,0.249590083068687));
#70468=CARTESIAN_POINT('Ctrl Pts',(-2.16153286152783,2.22405187279705,0.196969712698316));
#70469=CARTESIAN_POINT('Ctrl Pts',(-1.29099252632988,2.64857098947325,0.144349342327946));
#70470=CARTESIAN_POINT('Ctrl Pts',(-0.494964144347145,3.03675434170317,
0.0962328948852971));
#70471=CARTESIAN_POINT('Ctrl Pts',(0.493115753268411,3.03189109212113,0.0481164474426485));
#70472=CARTESIAN_POINT('Ctrl Pts',(1.29200104020318,2.64812001020929,-1.63834222883338E-16));
#70473=CARTESIAN_POINT('',(-1.28892185405328,2.64462557919715,0.));
#70474=CARTESIAN_POINT('Origin',(0.,0.,0.));
#70475=CARTESIAN_POINT('Ctrl Pts',(-1.28892185405328,2.64462557919715,2.08166817117217E-15));
#70476=CARTESIAN_POINT('Ctrl Pts',(-2.16403831185616,2.21811653527939,0.0526649636666859));
#70477=CARTESIAN_POINT('Ctrl Pts',(-2.80357657272064,1.32706756586464,0.10532992733337));
#70478=CARTESIAN_POINT('Ctrl Pts',(-2.92355402589586,0.366959843828546,
0.157994891000053));
#70479=CARTESIAN_POINT('Ctrl Pts',(-2.93861167702227,0.246462477535227,
0.164604554970166));
#70480=CARTESIAN_POINT('Ctrl Pts',(-2.94548559297357,0.124877349165528,
0.171214218940278));
#70481=CARTESIAN_POINT('Ctrl Pts',(-2.94453111094736,0.00313617179185542,
0.177823882910391));
#70482=CARTESIAN_POINT('Origin',(0.,0.,0.));
#70483=CARTESIAN_POINT('',(-2.93741501075088,0.000605053430647595,1.3221761170896));
#70484=CARTESIAN_POINT('',(-2.93743260967528,0.000720687897601403,1.17782388291039));
#70485=CARTESIAN_POINT('',(-2.942,-3.60291088309151E-16,0.));
#70486=CARTESIAN_POINT('Ctrl Pts',(-2.93741501075088,0.000605053430647595,
1.3221761170896));
#70487=CARTESIAN_POINT('Ctrl Pts',(-2.9382479568139,0.450815163107398,1.29790978476164));
#70488=CARTESIAN_POINT('Ctrl Pts',(-2.84099804532476,0.900683451883265,
1.27364345243368));
#70489=CARTESIAN_POINT('Ctrl Pts',(-2.64378204823906,1.30134356458571,1.24937712010572));
#70490=CARTESIAN_POINT('Ctrl Pts',(-2.21612867774369,2.17015567999336,1.19675674973535));
#70491=CARTESIAN_POINT('Ctrl Pts',(-1.31841648749453,2.80758195059898,1.14413637936498));
#70492=CARTESIAN_POINT('Ctrl Pts',(-0.357192829781819,2.92497002089294,
1.09151600899461));
#70493=CARTESIAN_POINT('Ctrl Pts',(0.604030827930888,3.04235809118689,1.03889563862424));
#70494=CARTESIAN_POINT('Ctrl Pts',(1.62876595310715,2.63970796116917,0.986275268253872));
#70495=CARTESIAN_POINT('Ctrl Pts',(2.25292793158662,1.89932766827126,0.933654897883501));
#70496=CARTESIAN_POINT('Ctrl Pts',(2.8770899100661,1.15894737537334,0.881034527513131));
#70497=CARTESIAN_POINT('Ctrl Pts',(3.1006787418488,0.0808369195952267,0.828414157142761));
#70498=CARTESIAN_POINT('Ctrl Pts',(2.82245137682484,-0.846673957408537,
0.775793786772391));
#70499=CARTESIAN_POINT('Ctrl Pts',(2.54422401180089,-1.7741848344123,0.72317341640202));
#70500=CARTESIAN_POINT('Ctrl Pts',(1.76418044997028,-2.55109613264171,0.67055304603165));
#70501=CARTESIAN_POINT('Ctrl Pts',(0.835554749603298,-2.82571794203434,
0.617932675661279));
#70502=CARTESIAN_POINT('Ctrl Pts',(-0.0930709507636752,-3.10033975142697,
0.565312305290909));
#70503=CARTESIAN_POINT('Ctrl Pts',(-1.17027878966702,-2.87267207198282,
0.512691934920538));
#70504=CARTESIAN_POINT('Ctrl Pts',(-1.90817450444562,-2.24552602141323,
0.460071564550168));
#70505=CARTESIAN_POINT('Ctrl Pts',(-2.55274401908064,-1.69769898118953,
0.414106415396644));
#70506=CARTESIAN_POINT('Ctrl Pts',(-2.93840347440061,-0.845052391620324,
0.368141266243119));
#70507=CARTESIAN_POINT('Ctrl Pts',(-2.94490570994055,0.00214417779480537,
0.322176117089595));
#70508=CARTESIAN_POINT('Ctrl Pts',(-2.94453111094736,0.00313617179185542,
0.177823882910391));
#70509=CARTESIAN_POINT('Ctrl Pts',(-2.93788040132423,-0.845140901703999,
0.223879182606963));
#70510=CARTESIAN_POINT('Ctrl Pts',(-2.55115114237882,-1.7009943502416,0.269934482303535));
#70511=CARTESIAN_POINT('Ctrl Pts',(-1.90455354763271,-2.24922658650796,
0.315989782000107));
#70512=CARTESIAN_POINT('Ctrl Pts',(-1.16515897070839,-2.87613882015091,
0.368654745666792));
#70513=CARTESIAN_POINT('Ctrl Pts',(-0.0859531713737992,-3.10079681277935,
0.421319709333476));
#70514=CARTESIAN_POINT('Ctrl Pts',(0.842833952810694,-2.82335342322726,
0.473984673000161));
#70515=CARTESIAN_POINT('Ctrl Pts',(1.77162107699519,-2.54591003367518,0.526649636666845));
#70516=CARTESIAN_POINT('Ctrl Pts',(2.54998952602959,-1.76636526194256,0.57931460033353));
#70517=CARTESIAN_POINT('Ctrl Pts',(2.82526196809064,-0.837265996441287,
0.631979564000215));
#70518=CARTESIAN_POINT('Ctrl Pts',(3.1005344101517,0.0918332690599885,0.684644527666899));
#70519=CARTESIAN_POINT('Ctrl Pts',(2.87271084523941,1.17048702832993,0.737309491333584));
#70520=CARTESIAN_POINT('Ctrl Pts',(2.2449320231631,1.90890163868963,0.789974455000268));
#70521=CARTESIAN_POINT('Ctrl Pts',(1.61715320108678,2.64731624904933,0.842639418666953));
#70522=CARTESIAN_POINT('Ctrl Pts',(0.589419121846451,3.0454917104988,0.895304382333637));
#70523=CARTESIAN_POINT('Ctrl Pts',(-0.37200976733393,2.9231058378395,0.947969346000322));
#70524=CARTESIAN_POINT('Ctrl Pts',(-1.33343865651431,2.8007199651802,1.00063430966701));
#70525=CARTESIAN_POINT('Ctrl Pts',(-2.22856235563474,2.15777275841214,1.05329927333369));
#70526=CARTESIAN_POINT('Ctrl Pts',(-2.6514251854394,1.28574400496261,1.10596423700038));
#70527=CARTESIAN_POINT('Ctrl Pts',(-2.8437527539192,0.889125626674557,1.12991745230371));
#70528=CARTESIAN_POINT('Ctrl Pts',(-2.93838674329414,0.445118617110292,
1.15387066760705));
#70529=CARTESIAN_POINT('Ctrl Pts',(-2.93743260967528,0.000720687897601403,
1.17782388291039));
#70530=CARTESIAN_POINT('Origin',(0.,0.,0.));
#70531=CARTESIAN_POINT('',(-2.94283216929169,-0.00254059509496668,2.3221761170896));
#70532=CARTESIAN_POINT('',(-2.94249560619114,-0.00258942729680482,2.17782388291039));
#70533=CARTESIAN_POINT('',(-2.942,-3.60291088309151E-16,0.));
#70534=CARTESIAN_POINT('Ctrl Pts',(-2.94283216929169,-0.00254059509496668,
2.3221761170896));
#70535=CARTESIAN_POINT('Ctrl Pts',(-2.93583836831966,0.770783310741536,
2.28029867365053));
#70536=CARTESIAN_POINT('Ctrl Pts',(-2.62244249954969,1.54912568223824,2.23842123021146));
#70537=CARTESIAN_POINT('Ctrl Pts',(-2.07534059520784,2.09189740289201,2.19654378677239));
#70538=CARTESIAN_POINT('Ctrl Pts',(-1.38788924974329,2.77390773164861,2.14392341640202));
#70539=CARTESIAN_POINT('Ctrl Pts',(-0.331445515483537,3.08398167899393,
2.09130304603165));
#70540=CARTESIAN_POINT('Ctrl Pts',(0.615553755286461,2.88169496582278,2.03868267566128));
#70541=CARTESIAN_POINT('Ctrl Pts',(1.56255302605646,2.67940825265162,1.98606230529091));
#70542=CARTESIAN_POINT('Ctrl Pts',(2.40010783333669,1.96476087896396,1.93344193492054));
#70543=CARTESIAN_POINT('Ctrl Pts',(2.74891040156469,1.06139789331815,1.88082156455017));
#70544=CARTESIAN_POINT('Ctrl Pts',(3.09771296979268,0.158034907672333,1.8282011941798));
#70545=CARTESIAN_POINT('Ctrl Pts',(2.95776329896845,-0.934043689931643,
1.77558082380943));
#70546=CARTESIAN_POINT('Ctrl Pts',(2.39244139669332,-1.72026117030417,1.72296045343906));
#70547=CARTESIAN_POINT('Ctrl Pts',(1.82711949441818,-2.50647865067671,1.67034008306869));
#70548=CARTESIAN_POINT('Ctrl Pts',(0.836425360692154,-2.9868350138178,1.61771971269832));
#70549=CARTESIAN_POINT('Ctrl Pts',(-0.130980997368149,-2.9437920444354,
1.56509934232795));
#70550=CARTESIAN_POINT('Ctrl Pts',(-1.09838735542844,-2.90074907505299,
1.51247897195758));
#70551=CARTESIAN_POINT('Ctrl Pts',(-2.04250593782301,-2.33430677314711,
1.45985860158721));
#70552=CARTESIAN_POINT('Ctrl Pts',(-2.5357679536495,-1.50098664208934,1.40723823121684));
#70553=CARTESIAN_POINT('Ctrl Pts',(-2.80155798635321,-1.05195919262036,
1.37888419317442));
#70554=CARTESIAN_POINT('Ctrl Pts',(-2.93644175348072,-0.525443729069001,
1.35053015513201));
#70555=CARTESIAN_POINT('Ctrl Pts',(-2.93741501075088,0.000605053430647595,
1.3221761170896));
#70556=CARTESIAN_POINT('Ctrl Pts',(-2.93743260967528,0.000720687897601403,
1.17782388291039));
#70557=CARTESIAN_POINT('Ctrl Pts',(-2.93628892837727,-0.53196109845813,
1.20653563127374));
#70558=CARTESIAN_POINT('Ctrl Pts',(-2.79780571115684,-1.06520455211536,
1.23524737963708));
#70559=CARTESIAN_POINT('Ctrl Pts',(-2.52560900690579,-1.51806949138664,
1.26395912800043));
#70560=CARTESIAN_POINT('Ctrl Pts',(-2.02632803807862,-2.34874393415536,
1.31662409166711));
#70561=CARTESIAN_POINT('Ctrl Pts',(-1.07716413993538,-2.9089825195618,1.3692890553338));
#70562=CARTESIAN_POINT('Ctrl Pts',(-0.108652539320438,-2.94471329972367,
1.42195401900048));
#70563=CARTESIAN_POINT('Ctrl Pts',(0.85985906129451,-2.98044407988555,1.47461898266717));
#70564=CARTESIAN_POINT('Ctrl Pts',(1.84771836438116,-2.49166705480286,1.52728394633385));
#70565=CARTESIAN_POINT('Ctrl Pts',(2.40686102399513,-1.70005997098112,1.57994891000054));
#70566=CARTESIAN_POINT('Ctrl Pts',(2.9660036836091,-0.908452887159384,1.63261387366722));
#70567=CARTESIAN_POINT('Ctrl Pts',(3.09642969975039,0.185984255401396,1.68527883733391));
#70568=CARTESIAN_POINT('Ctrl Pts',(2.73897659148843,1.08682694396802,1.73794380100059));
#70569=CARTESIAN_POINT('Ctrl Pts',(2.38152348322647,1.98766963253464,1.79060876466727));
#70570=CARTESIAN_POINT('Ctrl Pts',(1.53619125056127,2.69491786710711,1.84327372833396));
#70571=CARTESIAN_POINT('Ctrl Pts',(0.586406744725485,2.88778465426983,1.89593869200064));
#70572=CARTESIAN_POINT('Ctrl Pts',(-0.363377761110303,3.08065144143255,
1.94860365566733));
#70573=CARTESIAN_POINT('Ctrl Pts',(-1.41761454011667,2.75913678118554,2.00126861933401));
#70574=CARTESIAN_POINT('Ctrl Pts',(-2.09812527093809,2.0690698668059,2.0539335830007));
#70575=CARTESIAN_POINT('Ctrl Pts',(-2.63174175688638,1.52795998382732,2.09523034963726));
#70576=CARTESIAN_POINT('Ctrl Pts',(-2.93556254699721,0.76023565397735,2.13652711627383));
#70577=CARTESIAN_POINT('Ctrl Pts',(-2.94249560619114,-0.00258942729680482,
2.17782388291039));
#70578=CARTESIAN_POINT('Origin',(0.,0.,0.));
#70579=CARTESIAN_POINT('',(-2.94484294150901,0.00199174253909633,3.3221761170896));
#70580=CARTESIAN_POINT('',(-2.94526037616607,0.00180040430511289,3.17782388291039));
#70581=CARTESIAN_POINT('',(-2.942,-3.60291088309151E-16,0.));
#70582=CARTESIAN_POINT('Ctrl Pts',(-2.94484294150901,0.00199174253909633,
3.3221761170896));
#70583=CARTESIAN_POINT('Ctrl Pts',(-2.94583002736539,0.128597483532049,
3.31530793290979));
#70584=CARTESIAN_POINT('Ctrl Pts',(-2.93836342958051,0.255086036799256,
3.30843974872998));
#70585=CARTESIAN_POINT('Ctrl Pts',(-2.92204585589404,0.380422278131109,
3.30157156455017));
#70586=CARTESIAN_POINT('Ctrl Pts',(-2.79702929424561,1.34068182665933,3.2489511941798));
#70587=CARTESIAN_POINT('Ctrl Pts',(-2.15247739366928,2.23330287085301,3.19633082380943));
#70588=CARTESIAN_POINT('Ctrl Pts',(-1.28029158434589,2.65403966800756,3.14371045343906));
#70589=CARTESIAN_POINT('Ctrl Pts',(-0.4081057750225,3.0747764651621,3.09109008306869));
#70590=CARTESIAN_POINT('Ctrl Pts',(0.69171394304795,3.0236290152775,3.03846971269832));
#70591=CARTESIAN_POINT('Ctrl Pts',(1.5210867384019,2.5237607280468,2.98584934232795));
#70592=CARTESIAN_POINT('Ctrl Pts',(2.35045953375586,2.0238924408161,2.93322897195758));
#70593=CARTESIAN_POINT('Ctrl Pts',(2.90938540639331,1.07530331623929,2.8806086015872));
#70594=CARTESIAN_POINT('Ctrl Pts',(2.94474080948057,0.107585617606989,2.82798823121683));
#70595=CARTESIAN_POINT('Ctrl Pts',(2.98009621256783,-0.860132081025304,
2.77536786084646));
#70596=CARTESIAN_POINT('Ctrl Pts',(2.49188114610491,-1.84697835371309,2.7227474904761));
#70597=CARTESIAN_POINT('Ctrl Pts',(1.70119600494326,-2.40603518007504,2.67012712010573));
#70598=CARTESIAN_POINT('Ctrl Pts',(0.91051086378161,-2.965092006437,2.61750674973535));
#70599=CARTESIAN_POINT('Ctrl Pts',(-0.182644352078765,-3.09635938647313,
2.56488637936498));
#70600=CARTESIAN_POINT('Ctrl Pts',(-1.08320700768761,-2.74038967310636,
2.51226600899461));
#70601=CARTESIAN_POINT('Ctrl Pts',(-1.98376966329644,-2.3844199597396,2.45964563862424));
#70602=CARTESIAN_POINT('Ctrl Pts',(-2.69173975865374,-1.54121315296996,
2.40702526825387));
#70603=CARTESIAN_POINT('Ctrl Pts',(-2.88649532799773,-0.59263639450121,
2.3544048978835));
#70604=CARTESIAN_POINT('Ctrl Pts',(-2.92625644781122,-0.398975826678611,
2.3436619709522));
#70605=CARTESIAN_POINT('Ctrl Pts',(-2.94462630681883,-0.200923340849699,
2.3329190440209));
#70606=CARTESIAN_POINT('Ctrl Pts',(-2.94283216929169,-0.00254059509496668,
2.3221761170896));
#70607=CARTESIAN_POINT('Ctrl Pts',(-2.94249560619114,-0.00258942729680482,
2.17782388291039));
#70608=CARTESIAN_POINT('Ctrl Pts',(-2.94440414260591,-0.212580342560449,
2.18919207994051));
#70609=CARTESIAN_POINT('Ctrl Pts',(-2.92381470891138,-0.422199995772688,
2.20056027697063));
#70610=CARTESIAN_POINT('Ctrl Pts',(-2.87932772554241,-0.626618874207943,
2.21192847400075));
#70611=CARTESIAN_POINT('Ctrl Pts',(-2.67323476668884,-1.57362153232989,
2.26459343766743));
#70612=CARTESIAN_POINT('Ctrl Pts',(-1.95426416634525,-2.40900768006153,
2.31725840133412));
#70613=CARTESIAN_POINT('Ctrl Pts',(-1.04852602468143,-2.75386472764491,
2.3699233650008));
#70614=CARTESIAN_POINT('Ctrl Pts',(-0.142787883017607,-3.09872177522829,
2.42258832866749));
#70615=CARTESIAN_POINT('Ctrl Pts',(0.949717799966449,-2.95304972266342,
2.47525329233417));
#70616=CARTESIAN_POINT('Ctrl Pts',(1.7334537997702,-2.38292188563198,2.52791825600086));
#70617=CARTESIAN_POINT('Ctrl Pts',(2.51718979957395,-1.81279404860055,2.58058321966754));
#70618=CARTESIAN_POINT('Ctrl Pts',(2.99215611619739,-0.818210427102559,
2.63324818333423));
#70619=CARTESIAN_POINT('Ctrl Pts',(2.94291803037279,0.149706737509724,2.68591314700091));
#70620=CARTESIAN_POINT('Ctrl Pts',(2.89367994454819,1.11762390212201,2.7385781106676));
#70621=CARTESIAN_POINT('Ctrl Pts',(2.32023745627556,2.05887460984858,2.79124307433428));
#70622=CARTESIAN_POINT('Ctrl Pts',(1.4826919461771,2.54652764310569,2.84390803800096));
#70623=CARTESIAN_POINT('Ctrl Pts',(0.645146436078633,3.03418067636279,2.89657300166765));
#70624=CARTESIAN_POINT('Ctrl Pts',(-0.456502095845658,3.06823603515044,
2.94923796533433));
#70625=CARTESIAN_POINT('Ctrl Pts',(-1.32256928803916,2.63324686948073,3.00190292900102));
#70626=CARTESIAN_POINT('Ctrl Pts',(-2.18863648023266,2.19825770381101,3.0545678926677));
#70627=CARTESIAN_POINT('Ctrl Pts',(-2.81912233269536,1.29422401368392,3.10723285633439));
#70628=CARTESIAN_POINT('Ctrl Pts',(-2.92805183726137,0.331196319314338,
3.15989782000107));
#70629=CARTESIAN_POINT('Ctrl Pts',(-2.94041095304778,0.221931425219236,
3.16587317430418));
#70630=CARTESIAN_POINT('Ctrl Pts',(-2.94605601250203,0.111907094355046,
3.17184852860728));
#70631=CARTESIAN_POINT('Ctrl Pts',(-2.94526037616607,0.00180040430511289,
3.17782388291039));
#70632=CARTESIAN_POINT('Origin',(0.,0.,0.));
#70633=CARTESIAN_POINT('',(-2.93739242931988,0.000540407572186541,4.3221761170896));
#70634=CARTESIAN_POINT('',(-2.93753500859377,0.000882026442511373,4.17782388291039));
#70635=CARTESIAN_POINT('',(-2.942,-3.60291088309151E-16,0.));
#70636=CARTESIAN_POINT('Ctrl Pts',(-2.93739242931988,0.000540407572186541,
4.3221761170896));
#70637=CARTESIAN_POINT('Ctrl Pts',(-2.93814630501522,0.454709257120266,
4.29769682179868));
#70638=CARTESIAN_POINT('Ctrl Pts',(-2.83910536028106,0.908566671316128,
4.27321752650776));
#70639=CARTESIAN_POINT('Ctrl Pts',(-2.6385374625564,1.31194251096478,4.24873823121684));
#70640=CARTESIAN_POINT('Ctrl Pts',(-2.20739935432037,2.17903389691023,4.19611786084646));
#70641=CARTESIAN_POINT('Ctrl Pts',(-1.30713327152341,2.8128638865229,4.14349749047609));
#70642=CARTESIAN_POINT('Ctrl Pts',(-0.345447198709921,2.92638673563265,
4.09087712010572));
#70643=CARTESIAN_POINT('Ctrl Pts',(0.616238874103564,3.0399095847424,4.03825674973536));
#70644=CARTESIAN_POINT('Ctrl Pts',(1.63934493693357,2.63312529334921,3.98563637936499));
#70645=CARTESIAN_POINT('Ctrl Pts',(2.26053185174972,1.89025628960273,3.93301600899462));
#70646=CARTESIAN_POINT('Ctrl Pts',(2.88171876656588,1.14738728585625,3.88039563862425));
#70647=CARTESIAN_POINT('Ctrl Pts',(3.10098653336818,0.0684335697564567,
3.82777526825387));
#70648=CARTESIAN_POINT('Ctrl Pts',(2.8190342665149,-0.857973716122647,3.7751548978835));
#70649=CARTESIAN_POINT('Ctrl Pts',(2.53708199966161,-1.78438100200175,3.72253452751313));
#70650=CARTESIAN_POINT('Ctrl Pts',(1.75390969915275,-2.55824185766015,3.66991415714276));
#70651=CARTESIAN_POINT('Ctrl Pts',(0.824196505293748,-2.82909406262337,
3.61729378677239));
#70652=CARTESIAN_POINT('Ctrl Pts',(-0.105516688565254,-3.09994626758658,
3.56467341640202));
#70653=CARTESIAN_POINT('Ctrl Pts',(-1.18177077577439,-2.86778982185459,
3.51205304603165));
#70654=CARTESIAN_POINT('Ctrl Pts',(-1.91715720801869,-2.23776257255722,
3.45943267566128));
#70655=CARTESIAN_POINT('Ctrl Pts',(-2.55655857926025,-1.68996855643583,
3.41368048947072));
#70656=CARTESIAN_POINT('Ctrl Pts',(-2.93826750108625,-0.841388295482023,
3.36792830328016));
#70657=CARTESIAN_POINT('Ctrl Pts',(-2.94484294150901,0.00199174253909633,
3.3221761170896));
#70658=CARTESIAN_POINT('Ctrl Pts',(-2.94526037616607,0.00180040430511289,
3.17782388291039));
#70659=CARTESIAN_POINT('Ctrl Pts',(-2.93904351473207,-0.858539934689441,
3.22451349227397));
#70660=CARTESIAN_POINT('Ctrl Pts',(-2.53959728591596,-1.72390862024193,
3.27120310163755));
#70661=CARTESIAN_POINT('Ctrl Pts',(-1.87733008879233,-2.27130145042432,
3.31789271100113));
#70662=CARTESIAN_POINT('Ctrl Pts',(-1.13030567908798,-2.88874982718133,
3.37055767466781));
#70663=CARTESIAN_POINT('Ctrl Pts',(-0.0488837030099704,-3.10162488208327,
3.4232226383345));
#70664=CARTESIAN_POINT('Ctrl Pts',(0.876425794829888,-2.81337100100799,
3.47588760200118));
#70665=CARTESIAN_POINT('Ctrl Pts',(1.80173529266975,-2.5251171199327,3.52855256566786));
#70666=CARTESIAN_POINT('Ctrl Pts',(2.57093231227146,-1.73573430288019,3.58121752933455));
#70667=CARTESIAN_POINT('Ctrl Pts',(2.83512541526138,-0.803269840348294,
3.63388249300123));
#70668=CARTESIAN_POINT('Ctrl Pts',(3.0993185182513,0.129194622183599,3.68654745666792));
#70669=CARTESIAN_POINT('Ctrl Pts',(2.85850770462944,1.20474073019488,3.7392124203346));
#70670=CARTESIAN_POINT('Ctrl Pts',(2.22191964750238,1.93552360728328,3.79187738400129));
#70671=CARTESIAN_POINT('Ctrl Pts',(1.58533159037532,2.66630648437168,3.84454234766797));
#70672=CARTESIAN_POINT('Ctrl Pts',(0.552966289743035,3.05232613053722,3.89720731133465));
#70673=CARTESIAN_POINT('Ctrl Pts',(-0.406917273431679,2.91849222887777,
3.94987227500134));
#70674=CARTESIAN_POINT('Ctrl Pts',(-1.36680083660641,2.78465832721833,4.00253723866802));
#70675=CARTESIAN_POINT('Ctrl Pts',(-2.25420266232356,2.13097087773392,4.05520220233471));
#70676=CARTESIAN_POINT('Ctrl Pts',(-2.666616123304,1.25392862924115,4.10786716600139));
#70677=CARTESIAN_POINT('Ctrl Pts',(-2.84922387445754,0.865593310885713,
4.13118607163773));
#70678=CARTESIAN_POINT('Ctrl Pts',(-2.9387088904313,0.433468688742346,4.15450497727406));
#70679=CARTESIAN_POINT('Ctrl Pts',(-2.93753500859377,0.000882026442511374,
4.17782388291039));
#70680=CARTESIAN_POINT('Origin',(0.,0.,0.));
#70681=CARTESIAN_POINT('',(-2.94294893056736,-0.00252441656932667,5.3221761170896));
#70682=CARTESIAN_POINT('',(-2.94214529852914,-0.00261326515612426,5.1778238829104));
#70683=CARTESIAN_POINT('',(-2.942,-3.60291088309151E-16,0.));
#70684=CARTESIAN_POINT('Ctrl Pts',(-2.94294893056736,-0.00252441656932667,
5.3221761170896));
#70685=CARTESIAN_POINT('Ctrl Pts',(-2.93593381851913,0.774652637504292,
5.28008571068756));
#70686=CARTESIAN_POINT('Ctrl Pts',(-2.61899610205614,1.55689120032164,5.23799530428553));
#70687=CARTESIAN_POINT('Ctrl Pts',(-2.06692649506365,2.10021140779169,5.1959048978835));
#70688=CARTESIAN_POINT('Ctrl Pts',(-1.37674291943613,2.77945670358908,5.14328452751313));
#70689=CARTESIAN_POINT('Ctrl Pts',(-0.31906293568821,3.08528758407071,5.09066415714276));
#70690=CARTESIAN_POINT('Ctrl Pts',(0.627116654359043,2.8792008952563,5.03804378677239));
#70691=CARTESIAN_POINT('Ctrl Pts',(1.5732962444063,2.67311420644189,4.98542341640202));
#70692=CARTESIAN_POINT('Ctrl Pts',(2.4079754407529,1.95510994833143,4.93280304603165));
#70693=CARTESIAN_POINT('Ctrl Pts',(2.75314891878373,1.05035428518759,4.88018267566128));
#70694=CARTESIAN_POINT('Ctrl Pts',(3.09832239681456,0.145598622043775,4.82756230529091));
#70695=CARTESIAN_POINT('Ctrl Pts',(2.95399015652965,-0.945908446133409,
4.77494193492054));
#70696=CARTESIAN_POINT('Ctrl Pts',(2.38551665840565,-1.72985067733577,4.72232156455017));
#70697=CARTESIAN_POINT('Ctrl Pts',(1.81704316028163,-2.51379290853814,4.6697011941798));
#70698=CARTESIAN_POINT('Ctrl Pts',(0.824428404318513,-2.99017030276568,
4.61708082380943));
#70699=CARTESIAN_POINT('Ctrl Pts',(-0.142797221412707,-2.9432434569701,
4.56446045343906));
#70700=CARTESIAN_POINT('Ctrl Pts',(-1.11002284714393,-2.89631661117452,
4.51184008306869));
#70701=CARTESIAN_POINT('Ctrl Pts',(-2.05185934264326,-2.32608552535581,
4.45921971269832));
#70702=CARTESIAN_POINT('Ctrl Pts',(-2.54177252355539,-1.49079359130735,
4.40659934232795));
#70703=CARTESIAN_POINT('Ctrl Pts',(-2.80377530896762,-1.04408421119714,
4.3784582672485));
#70704=CARTESIAN_POINT('Ctrl Pts',(-2.93652578376122,-0.52156611314212,
4.35031719216905));
#70705=CARTESIAN_POINT('Ctrl Pts',(-2.93739242931988,0.000540407572186541,
4.3221761170896));
#70706=CARTESIAN_POINT('Ctrl Pts',(-2.93753500859377,0.000882026442511374,
4.17782388291039));
#70707=CARTESIAN_POINT('Ctrl Pts',(-2.93605771780397,-0.543513730930775,
4.20716994094074));
#70708=CARTESIAN_POINT('Ctrl Pts',(-2.79100052624987,-1.08864123864977,
4.23651599897109));
#70709=CARTESIAN_POINT('Ctrl Pts',(-2.50727405993036,-1.54814577624058,
4.26586205700145));
#70710=CARTESIAN_POINT('Ctrl Pts',(-1.99809343933257,-2.37278088572845,
4.31852702066813));
#70711=CARTESIAN_POINT('Ctrl Pts',(-1.04230710189327,-2.92165405720309,
4.37119198433482));
#70712=CARTESIAN_POINT('Ctrl Pts',(-0.0734394371752462,-2.94580807344744,
4.4238569480015));
#70713=CARTESIAN_POINT('Ctrl Pts',(0.895428227542791,-2.9699620896918,4.47652191166818));
#70714=CARTESIAN_POINT('Ctrl Pts',(1.87737721953956,-2.46939695070584,4.52918687533487));
#70715=CARTESIAN_POINT('Ctrl Pts',(2.427016324523,-1.67115837574717,4.58185183900155));
#70716=CARTESIAN_POINT('Ctrl Pts',(2.97665542950643,-0.872919800788501,
4.63451680266824));
#70717=CARTESIAN_POINT('Ctrl Pts',(3.09398464747655,0.22299221014288,4.68718176633492));
#70718=CARTESIAN_POINT('Ctrl Pts',(2.725785936287,1.11949523708763,4.73984673000161));
#70719=CARTESIAN_POINT('Ctrl Pts',(2.35758722509745,2.01599826403239,4.79251169366829));
#70720=CARTESIAN_POINT('Ctrl Pts',(1.50386058474821,2.71309230699052,4.84517665733498));
#70721=CARTESIAN_POINT('Ctrl Pts',(0.551838293166775,2.8945903085884,4.89784162100166));
#70722=CARTESIAN_POINT('Ctrl Pts',(-0.400183998414646,3.07608831018627,
4.95050658466835));
#70723=CARTESIAN_POINT('Ctrl Pts',(-1.45050194122825,2.74199027042391,5.00317154833503));
#70724=CARTESIAN_POINT('Ctrl Pts',(-2.12271361651498,2.04383596665945,5.05583651200172));
#70725=CARTESIAN_POINT('Ctrl Pts',(-2.64172618991724,1.50479316935294,5.09649896897128));
#70726=CARTESIAN_POINT('Ctrl Pts',(-2.93533688440644,0.748724173372516,
5.13716142594084));
#70727=CARTESIAN_POINT('Ctrl Pts',(-2.94214529852914,-0.00261326515612426,
5.1778238829104));
#70728=CARTESIAN_POINT('Origin',(0.,0.,0.));
#70729=CARTESIAN_POINT('',(-2.94474230559933,0.0020353165097306,6.3221761170896));
#70730=CARTESIAN_POINT('',(-2.94552589459255,0.00164462538419303,6.1778238829104));
#70731=CARTESIAN_POINT('',(-2.942,-3.60291088309151E-16,0.));
#70732=CARTESIAN_POINT('Ctrl Pts',(-2.94474230559933,0.0020353165097306,
6.3221761170896));
#70733=CARTESIAN_POINT('Ctrl Pts',(-2.94577608567865,0.132578411608025,
6.31509496994683));
#70734=CARTESIAN_POINT('Ctrl Pts',(-2.93783733482844,0.262995037552802,
6.30801382280405));
#70735=CARTESIAN_POINT('Ctrl Pts',(-2.92049520368276,0.39214902611321,6.30093267566128));
#70736=CARTESIAN_POINT('Ctrl Pts',(-2.79162493090094,1.35189898976081,6.24831230529091));
#70737=CARTESIAN_POINT('Ctrl Pts',(-2.1434950231737,2.24192544902223,6.19569193492054));
#70738=CARTESIAN_POINT('Ctrl Pts',(-1.26962729970534,2.65915768867859,6.14307156455017));
#70739=CARTESIAN_POINT('Ctrl Pts',(-0.395759576236975,3.07638992833495,
6.0904511941798));
#70740=CARTESIAN_POINT('Ctrl Pts',(0.70384596297251,3.02082794838624,6.03783082380943));
#70741=CARTESIAN_POINT('Ctrl Pts',(1.53120548099802,2.51763437940803,5.98521045343906));
#70742=CARTESIAN_POINT('Ctrl Pts',(2.35856499902354,2.0144408104298,5.93259008306869));
#70743=CARTESIAN_POINT('Ctrl Pts',(2.91367849586509,1.06361565242206,5.87996971269832));
#70744=CARTESIAN_POINT('Ctrl Pts',(2.9451489575673,0.0957638301017936,5.82734934232795));
#70745=CARTESIAN_POINT('Ctrl Pts',(2.97661941926951,-0.872087992218468,
5.77472897195758));
#70746=CARTESIAN_POINT('Ctrl Pts',(2.48444684583239,-1.85696647885126,5.72210860158721));
#70747=CARTESIAN_POINT('Ctrl Pts',(1.69152388176343,-2.41284480454905,5.66948823121684));
#70748=CARTESIAN_POINT('Ctrl Pts',(0.898600917694462,-2.96872313024685,
5.61686786084646));
#70749=CARTESIAN_POINT('Ctrl Pts',(-0.19507243700635,-3.09560129500965,
5.56424749047609));
#70750=CARTESIAN_POINT('Ctrl Pts',(-1.09419888335647,-2.73601935246765,
5.51162712010572));
#70751=CARTESIAN_POINT('Ctrl Pts',(-1.9933253297066,-2.37643740992565,5.45900674973535));
#70752=CARTESIAN_POINT('Ctrl Pts',(-2.69790486770603,-1.53039536007885,
5.40638637936499));
#70753=CARTESIAN_POINT('Ctrl Pts',(-2.88885105295217,-0.581044479598858,
5.35376600899461));
#70754=CARTESIAN_POINT('Ctrl Pts',(-2.92706166295704,-0.391068040923041,
5.34323604502627));
#70755=CARTESIAN_POINT('Ctrl Pts',(-2.94470393564848,-0.196954622309047,
5.33270608105794));
#70756=CARTESIAN_POINT('Ctrl Pts',(-2.94294893056736,-0.00252441656932667,
5.3221761170896));
#70757=CARTESIAN_POINT('Ctrl Pts',(-2.94214529852914,-0.00261326515612426,
5.1778238829104));
#70758=CARTESIAN_POINT('Ctrl Pts',(-2.94415496646843,-0.224388664623296,
5.18982638960752));
#70759=CARTESIAN_POINT('Ctrl Pts',(-2.92117618657372,-0.445751813963285,
5.20182889630465));
#70760=CARTESIAN_POINT('Ctrl Pts',(-2.87162987121487,-0.660999575716158,
5.21383140300177));
#70761=CARTESIAN_POINT('Ctrl Pts',(-2.65422904286817,-1.60547024656074,
5.26649636666845));
#70762=CARTESIAN_POINT('Ctrl Pts',(-1.92532197841492,-2.43220102048334,
5.31916133033513));
#70763=CARTESIAN_POINT('Ctrl Pts',(-1.01552544630456,-2.76620437138433,
5.37182629400182));
#70764=CARTESIAN_POINT('Ctrl Pts',(-0.105728914194198,-3.10020772228531,
5.4244912576685));
#70765=CARTESIAN_POINT('Ctrl Pts',(0.984957085573281,-2.94148365016469,
5.47715622133519));
#70766=CARTESIAN_POINT('Ctrl Pts',(1.761820540694,-2.36202602414577,5.52982118500188));
#70767=CARTESIAN_POINT('Ctrl Pts',(2.53868399581473,-1.78256839812686,5.58248614866856));
#70768=CARTESIAN_POINT('Ctrl Pts',(3.0017249062887,-0.782377218209647,5.63515111233524));
#70769=CARTESIAN_POINT('Ctrl Pts',(2.94091774630216,0.184882032222853,5.68781607600193));
#70770=CARTESIAN_POINT('Ctrl Pts',(2.88011058631563,1.15214128265535,5.74048103966861));
#70771=CARTESIAN_POINT('Ctrl Pts',(2.2954553558686,2.08646860360313,5.7931460033353));
#70772=CARTESIAN_POINT('Ctrl Pts',(1.45213925422783,2.56407295970403,5.84581096700198));
#70773=CARTESIAN_POINT('Ctrl Pts',(0.60882315258705,3.04167731580494,5.89847593066867));
#70774=CARTESIAN_POINT('Ctrl Pts',(-0.493153820247473,3.06255870705896,
5.95114089433535));
#70775=CARTESIAN_POINT('Ctrl Pts',(-1.35395830631657,2.6172457777424,6.00380585800203));
#70776=CARTESIAN_POINT('Ctrl Pts',(-2.21476279238567,2.17193284842583,6.05647082166872));
#70777=CARTESIAN_POINT('Ctrl Pts',(-2.83439479168936,1.26042559853868,6.10913578533541));
#70778=CARTESIAN_POINT('Ctrl Pts',(-2.93180238522596,0.296164363719765,
6.16180074900209));
#70779=CARTESIAN_POINT('Ctrl Pts',(-2.94168102690256,0.198373309905978,
6.1671417936382));
#70780=CARTESIAN_POINT('Ctrl Pts',(-2.94618853440423,0.100039675683843,
6.1724828382743));
#70781=CARTESIAN_POINT('Ctrl Pts',(-2.94552589459255,0.00164462538419303,
6.1778238829104));
#70782=CARTESIAN_POINT('Origin',(0.,0.,0.));
#70783=CARTESIAN_POINT('',(-2.93737184280031,0.000478285809368539,7.32217611708959));
#70784=CARTESIAN_POINT('',(-2.93765213932985,0.00105817779144944,7.17782388291039));
#70785=CARTESIAN_POINT('',(-2.942,-3.60291088309151E-16,0.));
#70786=CARTESIAN_POINT('Ctrl Pts',(-2.93737184280031,0.000478285809368539,
7.32217611708959));
#70787=CARTESIAN_POINT('Ctrl Pts',(-2.93804459091945,0.458606303769958,
7.29748385883571));
#70788=CARTESIAN_POINT('Ctrl Pts',(-2.83719423177179,0.916453996322869,
7.27279160058183));
#70789=CARTESIAN_POINT('Ctrl Pts',(-2.63324974290992,1.32252368027208,7.24809934232795));
#70790=CARTESIAN_POINT('Ctrl Pts',(-2.198634389848,2.18787738530332,7.19547897195758));
#70791=CARTESIAN_POINT('Ctrl Pts',(-1.29583121079705,2.81808837804428,7.14285860158721));
#70792=CARTESIAN_POINT('Ctrl Pts',(-0.333697177699206,2.92774986756231,
7.09023823121684));
#70793=CARTESIAN_POINT('Ctrl Pts',(0.628436855398639,3.03741135708034,7.03761786084647));
#70794=CARTESIAN_POINT('Ctrl Pts',(1.64990174254338,2.62652334337548,6.9849974904761));
#70795=CARTESIAN_POINT('Ctrl Pts',(2.26810159307568,1.88116672756646,6.93237712010573));
#70796=CARTESIAN_POINT('Ctrl Pts',(2.886301443608,1.13581011175742,6.87975674973536));
#70797=CARTESIAN_POINT('Ctrl Pts',(3.10123625752784,0.055984893844227,6.82713637936498));
#70798=CARTESIAN_POINT('Ctrl Pts',(2.81556743521199,-0.869283101865742,
6.77451600899461));
#70799=CARTESIAN_POINT('Ctrl Pts',(2.52989861289615,-1.7945510975757,6.72189563862424));
#70800=CARTESIAN_POINT('Ctrl Pts',(1.74362615434463,-2.56526187108243,6.66927526825387));
#70801=CARTESIAN_POINT('Ctrl Pts',(0.812833183747132,-2.8323797960046,6.6166548978835));
#70802=CARTESIAN_POINT('Ctrl Pts',(-0.117959786850361,-3.09949772092676,
6.56403452751313));
#70803=CARTESIAN_POINT('Ctrl Pts',(-1.19327326949384,-2.86302279726437,
6.51141415714276));
#70804=CARTESIAN_POINT('Ctrl Pts',(-1.92612469189739,-2.23004860141629,
6.45879378677239));
#70805=CARTESIAN_POINT('Ctrl Pts',(-2.56035596550109,-1.68225403062272,
6.41325456354479));
#70806=CARTESIAN_POINT('Ctrl Pts',(-2.93809401248361,-0.83749407451141,
6.3677153403172));
#70807=CARTESIAN_POINT('Ctrl Pts',(-2.94474230559933,0.0020353165097306,
6.3221761170896));
#70808=CARTESIAN_POINT('Ctrl Pts',(-2.94552589459255,0.00164462538419303,
6.1778238829104));
#70809=CARTESIAN_POINT('Ctrl Pts',(-2.93965462503178,-0.87017722046166,
6.22514780194098));
#70810=CARTESIAN_POINT('Ctrl Pts',(-2.52789003171806,-1.74682066505967,
6.27247172097156));
#70811=CARTESIAN_POINT('Ctrl Pts',(-1.85003983495055,-2.2935847848838,6.31979564000214));
#70812=CARTESIAN_POINT('Ctrl Pts',(-1.095686503369,-2.90205747891776,6.37246060366883));
#70813=CARTESIAN_POINT('Ctrl Pts',(-0.0117966524363787,-3.10198764723502,
6.42512556733551));
#70814=CARTESIAN_POINT('Ctrl Pts',(0.910000294361383,-2.80269121035772,
6.4777905310022));
#70815=CARTESIAN_POINT('Ctrl Pts',(1.83179724115916,-2.50339477348041,6.53045549466888));
#70816=CARTESIAN_POINT('Ctrl Pts',(2.59150128382206,-1.70487173140855,6.58312045833556));
#70817=CARTESIAN_POINT('Ctrl Pts',(2.8445267984577,-0.769315181970455,6.63578542200225));
#70818=CARTESIAN_POINT('Ctrl Pts',(3.09755231309333,0.166241367467632,6.68845038566893));
#70819=CARTESIAN_POINT('Ctrl Pts',(2.84389929970168,1.23883142427194,6.74111534933562));
#70820=CARTESIAN_POINT('Ctrl Pts',(2.19861937965545,1.96195091165853,6.79378031300231));
#70821=CARTESIAN_POINT('Ctrl Pts',(1.55333945960922,2.68507039904512,6.84644527666899));
#70822=CARTESIAN_POINT('Ctrl Pts',(0.51643263290838,3.05871931701401,6.89911024033567));
#70823=CARTESIAN_POINT('Ctrl Pts',(-0.441782179220013,2.91341844960141,
6.95177520400236));
#70824=CARTESIAN_POINT('Ctrl Pts',(-1.39999699134843,2.76811758218879,7.00444016766904));
#70825=CARTESIAN_POINT('Ctrl Pts',(-2.2795197889044,2.10386692939468,7.05710513133573));
#70826=CARTESIAN_POINT('Ctrl Pts',(-2.68141770473996,1.22195648411116,7.10977009500241));
#70827=CARTESIAN_POINT('Ctrl Pts',(-2.85452884366231,0.842087578115104,
7.13245469097174));
#70828=CARTESIAN_POINT('Ctrl Pts',(-2.93902534565796,0.421835844039577,
7.15513928694107));
#70829=CARTESIAN_POINT('Ctrl Pts',(-2.93765213932985,0.00105817779144944,
7.17782388291039));
#70830=CARTESIAN_POINT('Origin',(0.,0.,0.));
#70831=CARTESIAN_POINT('',(-2.94306537549688,-0.00250657139928612,8.3221761170896));
#70832=CARTESIAN_POINT('',(-2.94179645842688,-0.00262223567938445,8.17782388291039));
#70833=CARTESIAN_POINT('',(-2.942,-3.60291088309151E-16,0.));
#70834=CARTESIAN_POINT('Ctrl Pts',(-2.94306537549688,-0.00250657139928612,
8.3221761170896));
#70835=CARTESIAN_POINT('Ctrl Pts',(-2.93603346312234,0.778523040326291,
8.2798727477246));
#70836=CARTESIAN_POINT('Ctrl Pts',(-2.6155295502631,1.5646541741046,8.23756937835961));
#70837=CARTESIAN_POINT('Ctrl Pts',(-2.0584790752992,2.10849163858216,8.19526600899462));
#70838=CARTESIAN_POINT('Ctrl Pts',(-1.36557440251332,2.78496089461673,8.14264563862425));
#70839=CARTESIAN_POINT('Ctrl Pts',(-0.306675260078988,3.08654352280986,
8.09002526825387));
#70840=CARTESIAN_POINT('Ctrl Pts',(0.638669423716989,2.87666029635488,8.0374048978835));
#70841=CARTESIAN_POINT('Ctrl Pts',(1.58401410751295,2.66677706989991,7.98478452751313));
#70842=CARTESIAN_POINT('Ctrl Pts',(2.41580433267058,1.94542798879682,7.93216415714276));
#70843=CARTESIAN_POINT('Ctrl Pts',(2.75734311734437,1.03929400395132,7.87954378677239));
#70844=CARTESIAN_POINT('Ctrl Pts',(3.09888190201817,0.133160019105817,7.82692341640202));
#70845=CARTESIAN_POINT('Ctrl Pts',(2.95016924620815,-0.957758869482093,
7.77430304603165));
#70846=CARTESIAN_POINT('Ctrl Pts',(2.37855339098706,-1.73941279161662,7.72168267566128));
#70847=CARTESIAN_POINT('Ctrl Pts',(1.80693753576595,-2.52106671375116,7.66906230529091));
#70848=CARTESIAN_POINT('Ctrl Pts',(0.812418481133763,-2.99345566943229,
7.61644193492054));
#70849=CARTESIAN_POINT('Ctrl Pts',(-0.154610975618871,-2.94264651965433,
7.56382156455017));
#70850=CARTESIAN_POINT('Ctrl Pts',(-1.1216404323715,-2.89183736987637,7.5112011941798));
#70851=CARTESIAN_POINT('Ctrl Pts',(-2.06118029124457,-2.31783011463932,
7.45858082380943));
#70852=CARTESIAN_POINT('Ctrl Pts',(-2.54773645714466,-1.48057827836003,
7.40596045343906));
#70853=CARTESIAN_POINT('Ctrl Pts',(-2.80597476023112,-1.03620924430037,
7.37803234132257));
#70854=CARTESIAN_POINT('Ctrl Pts',(-2.93661093285418,-0.517686173583286,
7.35010422920608));
#70855=CARTESIAN_POINT('Ctrl Pts',(-2.93737184280031,0.000478285809368539,
7.32217611708959));
#70856=CARTESIAN_POINT('Ctrl Pts',(-2.93765213932985,0.00105817779144944,
7.17782388291039));
#70857=CARTESIAN_POINT('Ctrl Pts',(-2.93583728528984,-0.555049110608679,
7.20780425060775));
#70858=CARTESIAN_POINT('Ctrl Pts',(-2.78403605908896,-1.11207503097007,
7.23778461830511));
#70859=CARTESIAN_POINT('Ctrl Pts',(-2.48858495099342,-1.57801251517323,
7.26776498600247));
#70860=CARTESIAN_POINT('Ctrl Pts',(-1.96958124729618,-2.39650083140119,
7.32042994966915));
#70861=CARTESIAN_POINT('Ctrl Pts',(-1.00730080578659,-2.93390722608419,
7.37309491333584));
#70862=CARTESIAN_POINT('Ctrl Pts',(-0.0382136038189444,-2.94647556868157,
7.42575987700252));
#70863=CARTESIAN_POINT('Ctrl Pts',(0.930873598148709,-2.95904391127895,
7.47842484066921));
#70864=CARTESIAN_POINT('Ctrl Pts',(1.90676756057442,-2.44677420179069,7.53108980433588));
#70865=CARTESIAN_POINT('Ctrl Pts',(2.44682350205541,-1.64202110404938,7.58375476800257));
#70866=CARTESIAN_POINT('Ctrl Pts',(2.98687944353639,-0.837268006308086,
7.63641973166925));
#70867=CARTESIAN_POINT('Ctrl Pts',(3.09109736407267,0.25996847968624,7.68908469533594));
#70868=CARTESIAN_POINT('Ctrl Pts',(2.71220622763963,1.15200518015635,7.74174965900263));
#70869=CARTESIAN_POINT('Ctrl Pts',(2.33331509120659,2.04404188062646,7.79441462266931));
#70870=CARTESIAN_POINT('Ctrl Pts',(1.47131489780423,2.73087879557235,7.84707958633599));
#70871=CARTESIAN_POINT('Ctrl Pts',(0.517190633372317,2.90098128313613,7.89974455000268));
#70872=CARTESIAN_POINT('Ctrl Pts',(-0.436933631059594,3.07108377069992,
7.95240951366936));
#70873=CARTESIAN_POINT('Ctrl Pts',(-1.48318196652107,2.72445183088159,8.00507447733605));
#70874=CARTESIAN_POINT('Ctrl Pts',(-2.14699834174799,2.01831035197405,8.05773944100273));
#70875=CARTESIAN_POINT('Ctrl Pts',(-2.65153376339188,1.48160562142403,8.09776758830529));
#70876=CARTESIAN_POINT('Ctrl Pts',(-2.93514585523751,0.737219387421443,
8.13779573560784));
#70877=CARTESIAN_POINT('Ctrl Pts',(-2.94179645842688,-0.00262223567938445,
8.17782388291039));
#70878=CARTESIAN_POINT('Origin',(0.,0.,0.));
#70879=CARTESIAN_POINT('',(-2.94464008512449,0.00207742171232136,9.3221761170896));
#70880=CARTESIAN_POINT('',(-2.94577110767244,0.00147777103002609,9.1778238829104));
#70881=CARTESIAN_POINT('',(-2.942,-3.60291088309151E-16,0.));
#70882=CARTESIAN_POINT('Ctrl Pts',(-2.94464008512449,0.00207742171232136,
9.3221761170896));
#70883=CARTESIAN_POINT('Ctrl Pts',(-2.94572064417758,0.136558752036829,
9.31488200698387));
#70884=CARTESIAN_POINT('Ctrl Pts',(-2.93729508396668,0.270903986837675,
9.30758789687813));
#70885=CARTESIAN_POINT('Ctrl Pts',(-2.91889749004766,0.4038694541666,9.3002937867724));
#70886=CARTESIAN_POINT('Ctrl Pts',(-2.7861755826581,1.3630943679524,9.24767341640203));
#70887=CARTESIAN_POINT('Ctrl Pts',(-2.1344781113937,2.25051190295123,9.19505304603165));
#70888=CARTESIAN_POINT('Ctrl Pts',(-1.25894255572533,2.66423286046833,9.14243267566128));
#70889=CARTESIAN_POINT('Ctrl Pts',(-0.383407000056953,3.07795381798544,
9.08981230529091));
#70890=CARTESIAN_POINT('Ctrl Pts',(0.715966640015389,3.01797819802083,9.03719193492054));
#70891=CARTESIAN_POINT('Ctrl Pts',(1.54129954888374,2.51146745828537,8.98457156455017));
#70892=CARTESIAN_POINT('Ctrl Pts',(2.3666324577521,2.00495671854991,8.9319511941798));
#70893=CARTESIAN_POINT('Ctrl Pts',(2.91792463541645,1.05191085904358,8.87933082380943));
#70894=CARTESIAN_POINT('Ctrl Pts',(2.94550964776859,0.0839405046308018,
8.82671045343906));
#70895=CARTESIAN_POINT('Ctrl Pts',(2.97309466012074,-0.884029849781979,
8.77409008306869));
#70896=CARTESIAN_POINT('Ctrl Pts',(2.47697250716068,-1.86692469910122,8.72146971269832));
#70897=CARTESIAN_POINT('Ctrl Pts',(1.68182449914462,-2.41961555778857,8.66884934232795));
#70898=CARTESIAN_POINT('Ctrl Pts',(0.886676491128584,-2.97230641647591,
8.61622897195757));
#70899=CARTESIAN_POINT('Ctrl Pts',(-0.207497371943416,-3.09479328453138,
8.56360860158721));
#70900=CARTESIAN_POINT('Ctrl Pts',(-1.10517312337017,-2.73160492399537,
8.51098823121684));
#70901=CARTESIAN_POINT('Ctrl Pts',(-2.00284887479693,-2.36841656345936,
8.45836786084647));
#70902=CARTESIAN_POINT('Ctrl Pts',(-2.70402651457844,-1.51955297433185,
8.4057474904761));
#70903=CARTESIAN_POINT('Ctrl Pts',(-2.89116023290047,-0.56944323783011,
8.35312712010573));
#70904=CARTESIAN_POINT('Ctrl Pts',(-2.92785056302318,-0.383160187412328,
8.34281011910035));
#70905=CARTESIAN_POINT('Ctrl Pts',(-2.94478032747652,-0.192985093804385,
8.33249311809497));
#70906=CARTESIAN_POINT('Ctrl Pts',(-2.94306537549688,-0.00250657139928612,
8.3221761170896));
#70907=CARTESIAN_POINT('Ctrl Pts',(-2.94179645842688,-0.00262223567938445,
8.17782388291039));
#70908=CARTESIAN_POINT('Ctrl Pts',(-2.94389604226671,-0.236188947098698,
8.19046069927452));
#70909=CARTESIAN_POINT('Ctrl Pts',(-2.91839215134056,-0.469302718100354,
8.20309751563865));
#70910=CARTESIAN_POINT('Ctrl Pts',(-2.86352159037298,-0.695286025907358,
8.21573433200279));
#70911=CARTESIAN_POINT('Ctrl Pts',(-2.63484404877868,-1.63708990688444,
8.26839929566947));
#70912=CARTESIAN_POINT('Ctrl Pts',(-1.89610455059774,-2.45504665084187,
8.32106425933616));
#70913=CARTESIAN_POINT('Ctrl Pts',(-0.982379647459882,-2.77814844538783,
8.37372922300284));
#70914=CARTESIAN_POINT('Ctrl Pts',(-0.068654744322021,-3.1012502399338,
8.42639418666953));
#70915=CARTESIAN_POINT('Ctrl Pts',(1.02005556377276,-2.92949708506828,8.47905915033621));
#70916=CARTESIAN_POINT('Ctrl Pts',(1.78993539631662,-2.34079256521527,8.53172411400289));
#70917=CARTESIAN_POINT('Ctrl Pts',(2.55981522886048,-1.75208804536226,8.58438907766958));
#70918=CARTESIAN_POINT('Ctrl Pts',(3.01086458585342,-0.746432160521719,
8.63705404133626));
#70919=CARTESIAN_POINT('Ctrl Pts',(2.93849705553841,0.220030931794408,8.68971900500295));
#70920=CARTESIAN_POINT('Ctrl Pts',(2.86612952522341,1.18649402411053,8.74238396866963));
#70921=CARTESIAN_POINT('Ctrl Pts',(2.27034510760049,2.11376432390223,8.79504893233632));
#70922=CARTESIAN_POINT('Ctrl Pts',(1.42137896494728,2.58125171077128,8.847713896003));
#70923=CARTESIAN_POINT('Ctrl Pts',(0.572412822294062,3.04873909764032,8.90037885966968));
#70924=CARTESIAN_POINT('Ctrl Pts',(-0.529735045389435,3.05644357158669,
8.95304382333637));
#70925=CARTESIAN_POINT('Ctrl Pts',(-1.38515376586909,2.60087054680792,9.00570878700305));
#70926=CARTESIAN_POINT('Ctrl Pts',(-2.24057248634875,2.14529752202914,9.05837375066974));
#70927=CARTESIAN_POINT('Ctrl Pts',(-2.84926205962455,1.2264469985252,9.11103871433643));
#70928=CARTESIAN_POINT('Ctrl Pts',(-2.93513381881397,0.261090064936974,
9.16370367800311));
#70929=CARTESIAN_POINT('Ctrl Pts',(-2.94280828744918,0.174814884615283,
9.16841041297221));
#70930=CARTESIAN_POINT('Ctrl Pts',(-2.94630689264378,0.0881682471389342,
9.1731171479413));
#70931=CARTESIAN_POINT('Ctrl Pts',(-2.94577110767244,0.00147777103002609,
9.1778238829104));
#70932=CARTESIAN_POINT('Origin',(0.,0.,0.));
#70933=CARTESIAN_POINT('',(-2.93735377875815,0.0004158914717875,10.3221761170896));
#70934=CARTESIAN_POINT('',(-2.93779053274574,0.00122895754932335,10.1778238829104));
#70935=CARTESIAN_POINT('',(-2.942,-3.60291088309151E-16,0.));
#70936=CARTESIAN_POINT('Ctrl Pts',(-2.93735377875815,0.0004158914717875,
10.3221761170896));
#70937=CARTESIAN_POINT('Ctrl Pts',(-2.93794360094505,0.462502223744089,
10.2972708958728));
#70938=CARTESIAN_POINT('Ctrl Pts',(-2.83526550161259,0.924340675123848,
10.2723656746559));
#70939=CARTESIAN_POINT('Ctrl Pts',(-2.6279195904465,1.33308353810155,10.2474604534391));
#70940=CARTESIAN_POINT('Ctrl Pts',(-2.18983399605069,2.19668561771623,10.1948400830687));
#70941=CARTESIAN_POINT('Ctrl Pts',(-1.28450826872579,2.82326745826868,10.1422197126983));
#70942=CARTESIAN_POINT('Ctrl Pts',(-0.321941779407734,2.9290658210569,10.0895993423279));
#70943=CARTESIAN_POINT('Ctrl Pts',(0.640624709910309,3.03486418384512,10.0369789719576));
#70944=CARTESIAN_POINT('Ctrl Pts',(1.66043196122149,2.61987906886913,9.98435860158721));
#70945=CARTESIAN_POINT('Ctrl Pts',(2.27563478565877,1.87204685190273,9.93173823121684));
#70946=CARTESIAN_POINT('Ctrl Pts',(2.89083761009605,1.12421463493634,9.87911786084647));
#70947=CARTESIAN_POINT('Ctrl Pts',(3.10143600765941,0.0435353159795382,
9.82649749047609));
#70948=CARTESIAN_POINT('Ctrl Pts',(2.8120552331994,-0.880578479665677,9.77387712010572));
#70949=CARTESIAN_POINT('Ctrl Pts',(2.52267445873939,-1.8046922753109,9.72125674973535));
#70950=CARTESIAN_POINT('Ctrl Pts',(1.733314512256,-2.57224054764455,9.66863637936499));
#70951=CARTESIAN_POINT('Ctrl Pts',(0.801456763974427,-2.83561988794246,
9.61601600899462));
#70952=CARTESIAN_POINT('Ctrl Pts',(-0.130400984307143,-3.09899922824038,
9.56339563862425));
#70953=CARTESIAN_POINT('Ctrl Pts',(-1.20475653438691,-2.85820963650256,
9.51077526825387));
#70954=CARTESIAN_POINT('Ctrl Pts',(-1.93506113766943,-2.22229869434726,
9.4581548978835));
#70955=CARTESIAN_POINT('Ctrl Pts',(-2.5641326605009,-1.67453620870937,9.41282863761886));
#70956=CARTESIAN_POINT('Ctrl Pts',(-2.93792539338528,-0.833601734574448,
9.36750237735423));
#70957=CARTESIAN_POINT('Ctrl Pts',(-2.94464008512449,0.00207742171232136,
9.3221761170896));
#70958=CARTESIAN_POINT('Ctrl Pts',(-2.94577110767244,0.00147777103002609,
9.1778238829104));
#70959=CARTESIAN_POINT('Ctrl Pts',(-2.94031184592155,-0.881835546255158,
9.22578211160798));
#70960=CARTESIAN_POINT('Ctrl Pts',(-2.51599664630944,-1.76970025068938,
9.27374034030557));
#70961=CARTESIAN_POINT('Ctrl Pts',(-1.82248510748737,-2.31554023703778,
9.32169856900316));
#70962=CARTESIAN_POINT('Ctrl Pts',(-1.06091069186834,-2.91495026175178,
9.37436353266984));
#70963=CARTESIAN_POINT('Ctrl Pts',(0.0252920844727601,-3.1019069675073,
9.42702849633653));
#70964=CARTESIAN_POINT('Ctrl Pts',(0.943444704192239,-2.79161076199491,
9.47969346000322));
#70965=CARTESIAN_POINT('Ctrl Pts',(1.86159732391172,-2.48131455648253,9.5323584236699));
#70966=CARTESIAN_POINT('Ctrl Pts',(2.61169978700958,-1.67376543970224,9.58502338733658));
#70967=CARTESIAN_POINT('Ctrl Pts',(2.85352154222556,-0.735250545330611,
9.63768835100327));
#70968=CARTESIAN_POINT('Ctrl Pts',(3.09534329744155,0.203264349041017,9.69035331466995));
#70969=CARTESIAN_POINT('Ctrl Pts',(2.82888434477565,1.27274502100399,9.74301827833664));
#70970=CARTESIAN_POINT('Ctrl Pts',(2.17500480776272,1.98809774472063,9.79568324200333));
#70971=CARTESIAN_POINT('Ctrl Pts',(1.52112527074978,2.70345046843728,9.84834820567001));
#70972=CARTESIAN_POINT('Ctrl Pts',(0.479825149389799,3.06467524390761,9.90101316933669));
#70973=CARTESIAN_POINT('Ctrl Pts',(-0.476583929910364,2.90792818241875,
9.95367813300337));
#70974=CARTESIAN_POINT('Ctrl Pts',(-1.43299300921054,2.75118112092989,10.0063430966701));
#70975=CARTESIAN_POINT('Ctrl Pts',(-2.3045110464509,2.07646222248183,10.0590080603367));
#70976=CARTESIAN_POINT('Ctrl Pts',(-2.69583596380714,1.18980965393578,10.1116730240034));
#70977=CARTESIAN_POINT('Ctrl Pts',(-2.85967973895049,0.818577213506006,
10.1337233103058));
#70978=CARTESIAN_POINT('Ctrl Pts',(-2.93934508420187,0.410192546500391,
10.1557735966081));
#70979=CARTESIAN_POINT('Ctrl Pts',(-2.93779053274574,0.00122895754932335,
10.1778238829104));
#70980=CARTESIAN_POINT('Origin',(0.,0.,0.));
#70981=CARTESIAN_POINT('',(-2.94318142996902,-0.00248705772575741,11.3221761170896));
#70982=CARTESIAN_POINT('',(-2.94145083142593,-0.00261642954227547,11.1778238829104));
#70983=CARTESIAN_POINT('',(-2.942,-3.60291088309151E-16,0.));
#70984=CARTESIAN_POINT('Ctrl Pts',(-2.94318142996902,-0.00248705772575741,
11.3221761170896));
#70985=CARTESIAN_POINT('Ctrl Pts',(-2.93613735245544,0.782394524444463,
11.2796597847616));
#70986=CARTESIAN_POINT('Ctrl Pts',(-2.61204283140731,1.57241444895454,11.2371434524337));
#70987=CARTESIAN_POINT('Ctrl Pts',(-2.04999848462302,2.11673789269853,11.1946271201057));
#70988=CARTESIAN_POINT('Ctrl Pts',(-1.35438388023453,2.79042020824128,11.1420067497354));
#70989=CARTESIAN_POINT('Ctrl Pts',(-0.294282642636005,3.08774972424349,
11.089386379365));
#70990=CARTESIAN_POINT('Ctrl Pts',(0.65021190135765,2.87407334222539,11.0367660089946));
#70991=CARTESIAN_POINT('Ctrl Pts',(1.59470644535131,2.66039696020728,10.9841456386242));
#70992=CARTESIAN_POINT('Ctrl Pts',(2.42359429574009,1.93571468016887,10.9315252682539));
#70993=CARTESIAN_POINT('Ctrl Pts',(2.76149288344003,1.02821697529914,10.8789048978835));
#70994=CARTESIAN_POINT('Ctrl Pts',(3.09939147113997,0.120719270429434,10.8262845275131));
#70995=CARTESIAN_POINT('Ctrl Pts',(2.9463007961511,-0.969593859271576,10.7736641571428));
#70996=CARTESIAN_POINT('Ctrl Pts',(2.37155179497663,-1.74894687658982,10.7210437867724));
#70997=CARTESIAN_POINT('Ctrl Pts',(1.79680279380215,-2.52829989390807,10.668423416402));
#70998=CARTESIAN_POINT('Ctrl Pts',(0.800395466442055,-2.99669279884355,
10.6158030460317));
#70999=CARTESIAN_POINT('Ctrl Pts',(-0.166422238380945,-2.94200216382593,
10.5631826756613));
#71000=CARTESIAN_POINT('Ctrl Pts',(-1.13323994320395,-2.8873115288083,10.5105623052909));
#71001=CARTESIAN_POINT('Ctrl Pts',(-2.07046802548985,-2.30953735383759,
10.4579419349205));
#71002=CARTESIAN_POINT('Ctrl Pts',(-2.55365933589945,-1.47033910701379,
10.4053215645502));
#71003=CARTESIAN_POINT('Ctrl Pts',(-2.80815619982173,-1.02833338914462,
10.3776064153966));
#71004=CARTESIAN_POINT('Ctrl Pts',(-2.93669740996939,-0.513805263571333,
10.3498912662431));
#71005=CARTESIAN_POINT('Ctrl Pts',(-2.93735377875815,0.0004158914717875,
10.3221761170896));
#71006=CARTESIAN_POINT('Ctrl Pts',(-2.93779053274574,0.00122895754932335,
10.1778238829104));
#71007=CARTESIAN_POINT('Ctrl Pts',(-2.93563218928374,-0.566577199606596,
10.2084385602748));
#71008=CARTESIAN_POINT('Ctrl Pts',(-2.77690932929649,-1.13549932265473,
10.2390532376391));
#71009=CARTESIAN_POINT('Ctrl Pts',(-2.46954008606165,-1.60765366907442,
10.2696679150035));
#71010=CARTESIAN_POINT('Ctrl Pts',(-1.94078749348779,-2.41987818489459,
10.3223328786702));
#71011=CARTESIAN_POINT('Ctrl Pts',(-0.972150510867944,-2.9457409778909,
10.3749978423368));
#71012=CARTESIAN_POINT('Ctrl Pts',(-0.00298230764251388,-2.94672185015728,
10.4276628060035));
#71013=CARTESIAN_POINT('Ctrl Pts',(0.966185895582889,-2.94770272242366,
10.4803277696702));
#71014=CARTESIAN_POINT('Ctrl Pts',(1.93588531941386,-2.42380167396015,10.5329927333369));
#71015=CARTESIAN_POINT('Ctrl Pts',(2.46628089363149,-1.61264909700348,10.5856576970036));
#71016=CARTESIAN_POINT('Ctrl Pts',(2.99667646784912,-0.801496520046785,
10.6383226606703));
#71017=CARTESIAN_POINT('Ctrl Pts',(3.08776819245338,0.296907585403119,10.690987624337));
#71018=CARTESIAN_POINT('Ctrl Pts',(2.69823879520542,1.18435043817229,10.7436525880036));
#71019=CARTESIAN_POINT('Ctrl Pts',(2.30870939795745,2.07179329094149,10.7963175516703));
#71020=CARTESIAN_POINT('Ctrl Pts',(1.43855887885726,2.74827489102996,10.848982515337));
#71021=CARTESIAN_POINT('Ctrl Pts',(0.482469038528927,2.90695754754173,10.9016474790037));
#71022=CARTESIAN_POINT('Ctrl Pts',(-0.473620801799363,3.0656402040535,10.9543124426704));
#71023=CARTESIAN_POINT('Ctrl Pts',(-1.51564996335577,2.70652391698861,11.0069774063371));
#71024=CARTESIAN_POINT('Ctrl Pts',(-2.17097614256679,1.99249620947818,11.0596423700038));
#71025=CARTESIAN_POINT('Ctrl Pts',(-2.66116565955863,1.45839745352016,11.0990362076393));
#71026=CARTESIAN_POINT('Ctrl Pts',(-2.93498842496261,0.725719853723158,
11.1384300452748));
#71027=CARTESIAN_POINT('Ctrl Pts',(-2.94145083142593,-0.00261642954227547,
11.1778238829104));
#71028=CARTESIAN_POINT('Origin',(0.,0.,0.));
#71029=CARTESIAN_POINT('',(-2.9445363666432,0.00211803469319205,12.3221761170896));
#71030=CARTESIAN_POINT('',(-2.94599368555865,0.00130075687149912,12.1778238829104));
#71031=CARTESIAN_POINT('',(-2.942,-3.60291088309151E-16,0.));
#71032=CARTESIAN_POINT('Ctrl Pts',(-2.9445363666432,0.00211803469319205,
12.3221761170896));
#71033=CARTESIAN_POINT('Ctrl Pts',(-2.9456637214079,0.140538485345201,12.3146690440209));
#71034=CARTESIAN_POINT('Ctrl Pts',(-2.93673667551181,0.278812877817704,
12.3071619709522));
#71035=CARTESIAN_POINT('Ctrl Pts',(-2.91725274860024,0.415583368023806,
12.2996548978835));
#71036=CARTESIAN_POINT('Ctrl Pts',(-2.78068135240184,1.37426776932391,12.2470345275131));
#71037=CARTESIAN_POINT('Ctrl Pts',(-2.12542680364205,2.25906209195984,12.1944141571428));
#71038=CARTESIAN_POINT('Ctrl Pts',(-1.24823752065428,2.66926510338839,12.1417937867724));
#71039=CARTESIAN_POINT('Ctrl Pts',(-0.371048237666502,3.07946811481694,
12.089173416402));
#71040=CARTESIAN_POINT('Ctrl Pts',(0.728075779549269,3.01507981503809,12.0365530460316));
#71041=CARTESIAN_POINT('Ctrl Pts',(1.55136877770631,2.50526006508935,11.9839326756613));
#71042=CARTESIAN_POINT('Ctrl Pts',(2.37466177586334,1.99544031514062,11.9313123052909));
#71043=CARTESIAN_POINT('Ctrl Pts',(2.92212375496165,1.04018911502201,11.8786919349205));
#71044=CARTESIAN_POINT('Ctrl Pts',(2.9458228744686,0.0721158274039949,11.8260715645502));
#71045=CARTESIAN_POINT('Ctrl Pts',(2.96952199397554,-0.895957460214037,
11.7734511941798));
#71046=CARTESIAN_POINT('Ctrl Pts',(2.4694582538911,-1.87685283533148,11.7208308238094));
#71047=CARTESIAN_POINT('Ctrl Pts',(1.67209801460167,-2.42634732122405,11.6682104534391));
#71048=CARTESIAN_POINT('Ctrl Pts',(0.874737775312261,-2.9758418071166,11.6155900830687));
#71049=CARTESIAN_POINT('Ctrl Pts',(-0.219918963182118,-3.09393540378431,
11.5629697126983));
#71050=CARTESIAN_POINT('Ctrl Pts',(-1.11612955404462,-2.72714647754463,
11.510349342328));
#71051=CARTESIAN_POINT('Ctrl Pts',(-2.01234014490716,-2.36035755130494,
11.4577289719576));
#71052=CARTESIAN_POINT('Ctrl Pts',(-2.7101045881378,-1.50868610215784,11.4051086015872));
#71053=CARTESIAN_POINT('Ctrl Pts',(-2.89342282416388,-0.557832820042644,
11.3524882312168));
#71054=CARTESIAN_POINT('Ctrl Pts',(-2.9286231547134,-0.375252240171749,
11.3423841931744));
#71055=CARTESIAN_POINT('Ctrl Pts',(-2.94485546023631,-0.189014750280763,
11.332280155132));
#71056=CARTESIAN_POINT('Ctrl Pts',(-2.94318142996902,-0.00248705772575741,
11.3221761170896));
#71057=CARTESIAN_POINT('Ctrl Pts',(-2.94145083142593,-0.00261642954227547,
11.1778238829104));
#71058=CARTESIAN_POINT('Ctrl Pts',(-2.94362790824268,-0.247980760321293,
11.1910950089415));
#71059=CARTESIAN_POINT('Ctrl Pts',(-2.9154621622164,-0.492852393533084,
11.2043661349727));
#71060=CARTESIAN_POINT('Ctrl Pts',(-2.85500395443405,-0.729473081400432,
11.2176372610038));
#71061=CARTESIAN_POINT('Ctrl Pts',(-2.61508239022462,-1.6684755368126,11.2703022246705));
#71062=CARTESIAN_POINT('Ctrl Pts',(-1.86661606494013,-2.4775413196809,11.3229671883372));
#71063=CARTESIAN_POINT('Ctrl Pts',(-0.949093412422085,-2.7896953688222,
11.3756321520039));
#71064=CARTESIAN_POINT('Ctrl Pts',(-0.0315707599040525,-3.10184941796349,
11.4282971156705));
#71065=CARTESIAN_POINT('Ctrl Pts',(1.05500821984753,-2.91709173337779,11.4809620793372));
#71066=CARTESIAN_POINT('Ctrl Pts',(1.81779437152408,-2.31922447800469,11.5336270430039));
#71067=CARTESIAN_POINT('Ctrl Pts',(2.58058052320064,-1.7213572226316,11.5862920066706));
#71068=CARTESIAN_POINT('Ctrl Pts',(3.01957384680218,-0.710380396471107,
11.6389569703373));
#71069=CARTESIAN_POINT('Ctrl Pts',(2.93565629151018,0.255148376847553,11.691621934004));
#71070=CARTESIAN_POINT('Ctrl Pts',(2.85173873621817,1.22067715016623,11.7442868976707));
#71071=CARTESIAN_POINT('Ctrl Pts',(2.24491030203262,2.14075787064307,11.7969518613373));
#71072=CARTESIAN_POINT('Ctrl Pts',(1.39041548234847,2.59806145861508,11.849616825004));
#71073=CARTESIAN_POINT('Ctrl Pts',(0.535920662664327,3.05536504658708,11.9022817886707));
#71074=CARTESIAN_POINT('Ctrl Pts',(-0.566240542518395,3.04989150205426,
11.9549467523374));
#71075=CARTESIAN_POINT('Ctrl Pts',(-1.41615121076395,2.58412350821102,12.0076117160041));
#71076=CARTESIAN_POINT('Ctrl Pts',(-2.26606187900951,2.11835551436778,12.0602766796708));
#71077=CARTESIAN_POINT('Ctrl Pts',(-2.86372201031791,1.19229307121411,12.1129416433374));
#71078=CARTESIAN_POINT('Ctrl Pts',(-2.93804565964555,0.22597844177242,12.1656066070041));
#71079=CARTESIAN_POINT('Ctrl Pts',(-2.94379288681505,0.151256200025011,
12.1696790323062));
#71080=CARTESIAN_POINT('Ctrl Pts',(-2.94641083929854,0.0762932715455572,
12.1737514576083));
#71081=CARTESIAN_POINT('Ctrl Pts',(-2.94599368555865,0.00130075687149912,
12.1778238829104));
#71082=CARTESIAN_POINT('Origin',(0.,0.,0.));
#71083=CARTESIAN_POINT('',(-2.93733773658367,0.000353650820144602,13.3221761170896));
#71084=CARTESIAN_POINT('',(-2.93794966127546,0.0013934910171998,13.1778238829104));
#71085=CARTESIAN_POINT('',(-2.942,-3.60291088309151E-16,0.));
#71086=CARTESIAN_POINT('Ctrl Pts',(-2.93733773658367,0.000353650820144602,
13.3221761170896));
#71087=CARTESIAN_POINT('Ctrl Pts',(-2.93784318272048,0.466397170874405,
13.2970579329098));
#71088=CARTESIAN_POINT('Ctrl Pts',(-2.8333193685149,0.932226520914598,13.27193974873));
#71089=CARTESIAN_POINT('Ctrl Pts',(-2.62254748003497,1.34362161549686,13.2468215645502));
#71090=CARTESIAN_POINT('Ctrl Pts',(-2.18099904818651,2.20545788879211,13.1942011941798));
#71091=CARTESIAN_POINT('Ctrl Pts',(-1.27316460447925,2.82840106158337,13.1415808238094));
#71092=CARTESIAN_POINT('Ctrl Pts',(-0.31018098965669,2.93033473129373,13.0889604534391));
#71093=CARTESIAN_POINT('Ctrl Pts',(0.652802625165875,3.03226840100409,13.0363400830687));
#71094=CARTESIAN_POINT('Ctrl Pts',(1.67093541110377,2.61319256763355,12.9837197126983));
#71095=CARTESIAN_POINT('Ctrl Pts',(2.28313120153524,1.86289672775273,12.9310993423279));
#71096=CARTESIAN_POINT('Ctrl Pts',(2.89532699196672,1.1126008878719,12.8784789719576));
#71097=CARTESIAN_POINT('Ctrl Pts',(3.10158578689178,0.0310850414808014,
12.8258586015872));
#71098=CARTESIAN_POINT('Ctrl Pts',(2.80849777284497,-0.891859624755379,
12.7732382312168));
#71099=CARTESIAN_POINT('Ctrl Pts',(2.51540975879817,-1.81480429099155,12.7206178608465));
#71100=CARTESIAN_POINT('Ctrl Pts',(1.72297493577951,-2.57917777707278,12.6679974904761));
#71101=CARTESIAN_POINT('Ctrl Pts',(0.790067400131255,-2.83881430845519,
12.6153771201057));
#71102=CARTESIAN_POINT('Ctrl Pts',(-0.142840135516982,-3.0984508398376,
12.5627567497353));
#71103=CARTESIAN_POINT('Ctrl Pts',(-1.21622038379481,-2.85335041652122,
12.510136379365));
#71104=CARTESIAN_POINT('Ctrl Pts',(-1.94396638611522,-2.21451296488091,
12.4575160089946));
#71105=CARTESIAN_POINT('Ctrl Pts',(-2.56788867194677,-1.66681511174075,
12.4124027116929));
#71106=CARTESIAN_POINT('Ctrl Pts',(-2.93776159700942,-0.829711212970877,
12.3672894143913));
#71107=CARTESIAN_POINT('Ctrl Pts',(-2.9445363666432,0.00211803469319205,
12.3221761170896));
#71108=CARTESIAN_POINT('Ctrl Pts',(-2.94599368555865,0.00130075687149912,
12.1778238829104));
#71109=CARTESIAN_POINT('Ctrl Pts',(-2.94101617029297,-0.893516551252978,
12.226416421275));
#71110=CARTESIAN_POINT('Ctrl Pts',(-2.50391622116005,-1.79254618589271,
12.2750089596396));
#71111=CARTESIAN_POINT('Ctrl Pts',(-1.79466984706922,-2.33716467042755,
12.3236014980042));
#71112=CARTESIAN_POINT('Ctrl Pts',(-1.02598321781837,-2.92742633745608,
12.3762664616709));
#71113=CARTESIAN_POINT('Ctrl Pts',(0.0623772080302214,-3.10138285578342,
12.4289314253375));
#71114=CARTESIAN_POINT('Ctrl Pts',(0.976754244976282,-2.78013123936204,
12.4815963890042));
#71115=CARTESIAN_POINT('Ctrl Pts',(1.89113128192235,-2.45887962294065,12.5342613526709));
#71116=CARTESIAN_POINT('Ctrl Pts',(2.6315249299659,-1.64241987177053,12.5869263163376));
#71117=CARTESIAN_POINT('Ctrl Pts',(2.86210835815027,-0.701080799331296,
12.6395912800043));
#71118=CARTESIAN_POINT('Ctrl Pts',(3.09269178633465,0.240258273107937,12.692256243671));
#71119=CARTESIAN_POINT('Ctrl Pts',(2.81346499465986,1.30647666681628,12.7449212073377));
#71120=CARTESIAN_POINT('Ctrl Pts',(2.15107931219979,2.01396036610533,12.7975861710043));
#71121=CARTESIAN_POINT('Ctrl Pts',(1.48869362973973,2.72144406539436,12.850251134671));
#71122=CARTESIAN_POINT('Ctrl Pts',(0.443149056494409,3.07019307026412,12.9029160983377));
#71123=CARTESIAN_POINT('Ctrl Pts',(-0.511317558922748,2.90202221756343,
12.9555810620044));
#71124=CARTESIAN_POINT('Ctrl Pts',(-1.46578417433991,2.73385136486274,13.0082460256711));
#71125=CARTESIAN_POINT('Ctrl Pts',(-2.3291728319289,2.04876065459161,13.0609109893378));
#71126=CARTESIAN_POINT('Ctrl Pts',(-2.7098688231833,1.1574927237348,13.1135759530044));
#71127=CARTESIAN_POINT('Ctrl Pts',(-2.86467717936984,0.795062526234979,
13.1349919296398));
#71128=CARTESIAN_POINT('Ctrl Pts',(-2.93966715879244,0.398538727939818,
13.1564079062751));
#71129=CARTESIAN_POINT('Ctrl Pts',(-2.93794966127546,0.0013934910171998,
13.1778238829104));
#71130=CARTESIAN_POINT('Origin',(0.,0.,0.));
#71131=CARTESIAN_POINT('',(-2.94325266537063,-0.0024318079996577,14.3221761170896));
#71132=CARTESIAN_POINT('',(-2.94111188951679,-0.00259486169482749,14.1778238829104));
#71133=CARTESIAN_POINT('',(-2.942,-3.60291088309151E-16,0.));
#71134=CARTESIAN_POINT('Ctrl Pts',(-2.94325266537063,-0.0024318079996577,
14.3221761170896));
#71135=CARTESIAN_POINT('Ctrl Pts',(-2.93620194204164,0.786300619982285,
14.2794468217987));
#71136=CARTESIAN_POINT('Ctrl Pts',(-2.60854122084458,1.58016790859219,14.2367175265078));
#71137=CARTESIAN_POINT('Ctrl Pts',(-2.04150376744995,2.12493551247607,14.1939882312168));
#71138=CARTESIAN_POINT('Ctrl Pts',(-1.34320718641939,2.79580716825642,14.1413678608465));
#71139=CARTESIAN_POINT('Ctrl Pts',(-0.281884150596186,3.08890703892681,
14.0887474904761));
#71140=CARTESIAN_POINT('Ctrl Pts',(0.661753798897932,2.87144767774516,14.0361271201057));
#71141=CARTESIAN_POINT('Ctrl Pts',(1.60539174839208,2.65398831656351,13.9835067497354));
#71142=CARTESIAN_POINT('Ctrl Pts',(2.43134461155714,1.92596972352975,13.930886379365));
#71143=CARTESIAN_POINT('Ctrl Pts',(2.76559296922098,1.01711939779235,13.8782660089946));
#71144=CARTESIAN_POINT('Ctrl Pts',(3.09984132688481,0.108269072054953,13.8256456386242));
#71145=CARTESIAN_POINT('Ctrl Pts',(2.94238517904746,-0.981412986386104,
13.7730252682539));
#71146=CARTESIAN_POINT('Ctrl Pts',(2.36451469520878,-1.75845069530582,13.7204048978835));
#71147=CARTESIAN_POINT('Ctrl Pts',(1.7866442113701,-2.53548840422553,13.6677845275131));
#71148=CARTESIAN_POINT('Ctrl Pts',(0.788359391530092,-2.99988176362388,
13.6151641571428));
#71149=CARTESIAN_POINT('Ctrl Pts',(-0.178232238982059,-2.94131149038551,
13.5625437867724));
#71150=CARTESIAN_POINT('Ctrl Pts',(-1.14482386949421,-2.88274121714715,
13.509923416402));
#71151=CARTESIAN_POINT('Ctrl Pts',(-2.07972231067849,-2.30120731127206,
13.4573030460317));
#71152=CARTESIAN_POINT('Ctrl Pts',(-2.5595403212758,-1.46007567143488,13.4046826756613));
#71153=CARTESIAN_POINT('Ctrl Pts',(-2.81031856879004,-1.02045582826861,
13.3771804894707));
#71154=CARTESIAN_POINT('Ctrl Pts',(-2.9367843178467,-0.509922711901109,
13.3496783032802));
#71155=CARTESIAN_POINT('Ctrl Pts',(-2.93733773658367,0.000353650820144602,
13.3221761170896));
#71156=CARTESIAN_POINT('Ctrl Pts',(-2.93794966127546,0.0013934910171998,
13.1778238829104));
#71157=CARTESIAN_POINT('Ctrl Pts',(-2.9354435856223,-0.578098472832708,
13.2090728699418));
#71158=CARTESIAN_POINT('Ctrl Pts',(-2.76961959866241,-1.15891354184382,
13.2403218569731));
#71159=CARTESIAN_POINT('Ctrl Pts',(-2.45014221851649,-1.63706498032062,
13.2715708440045));
#71160=CARTESIAN_POINT('Ctrl Pts',(-1.91171629767549,-2.44290960207673,
13.3242358076712));
#71161=CARTESIAN_POINT('Ctrl Pts',(-0.936861131073665,-2.95715369414646,
13.3769007713379));
#71162=CARTESIAN_POINT('Ctrl Pts',(0.032249473718084,-2.94654692146698,
13.4295657350046));
#71163=CARTESIAN_POINT('Ctrl Pts',(1.00136007850986,-2.9359401487875,13.4822306986712));
#71164=CARTESIAN_POINT('Ctrl Pts',(1.96472612149158,-2.40048251135878,13.5348956623379));
#71165=CARTESIAN_POINT('Ctrl Pts',(2.48538560527679,-1.58304647931889,13.5875606260046));
#71166=CARTESIAN_POINT('Ctrl Pts',(3.00604508906198,-0.765610447279041,
13.6402255896713));
#71167=CARTESIAN_POINT('Ctrl Pts',(3.08399801365073,0.333803979371919,13.692890553338));
#71168=CARTESIAN_POINT('Ctrl Pts',(2.68388585052197,1.21652624548705,13.7455555170047));
#71169=CARTESIAN_POINT('Ctrl Pts',(2.28377368739319,2.0992485116022,13.7982204806713));
#71170=CARTESIAN_POINT('Ctrl Pts',(1.40559643654686,2.76527861718149,13.850885444338));
#71171=CARTESIAN_POINT('Ctrl Pts',(0.447678061833244,2.91251851826326,13.9035504080047));
#71172=CARTESIAN_POINT('Ctrl Pts',(-0.510240312880357,3.05975841934504,
13.9562153716714));
#71173=CARTESIAN_POINT('Ctrl Pts',(-1.54789981146125,2.68820811592931,14.0088803353381));
#71174=CARTESIAN_POINT('Ctrl Pts',(-2.1946428070508,1.96639671204873,14.0615452990048));
#71175=CARTESIAN_POINT('Ctrl Pts',(-2.67062249982462,1.435169358057,14.1003048269733));
#71176=CARTESIAN_POINT('Ctrl Pts',(-2.93486488519192,0.714225423327012,
14.1390643549419));
#71177=CARTESIAN_POINT('Ctrl Pts',(-2.94111188951679,-0.00259486169482749,
14.1778238829104));
#71178=CARTESIAN_POINT('Origin',(0.,0.,-1.84858989190501));
#71179=CARTESIAN_POINT('',(-2.37275986033066,-0.00196044888638088,14.651410108095));
#71180=CARTESIAN_POINT('',(-2.37517539399571,0.0009292342096269,14.848589891905));
#71181=CARTESIAN_POINT('',(-2.37175,-2.62313128856983E-13,-1.84858989190501));
#71182=CARTESIAN_POINT('',(-2.34668236863853,0.343918483395512,15.62825));
#71183=CARTESIAN_POINT('Ctrl Pts',(-2.37275986033066,-0.00196044888638126,
14.651410108095));
#71184=CARTESIAN_POINT('Ctrl Pts',(-2.37407562336888,-0.149148890039704,
14.6613011831744));
#71185=CARTESIAN_POINT('Ctrl Pts',(-2.29486163858049,-1.07797575416432,
14.7238126286243));
#71186=CARTESIAN_POINT('Ctrl Pts',(-1.07036982067409,-2.58532778276268,
14.8389444444444));
#71187=CARTESIAN_POINT('Ctrl Pts',(1.57881200919325,-2.30987053095853,14.9968055555556));
#71188=CARTESIAN_POINT('Ctrl Pts',(2.79654399706859,0.0566462213665858,
15.1546666666667));
#71189=CARTESIAN_POINT('Ctrl Pts',(1.48409012818578,2.37398300468726,15.3125277777778));
#71190=CARTESIAN_POINT('Ctrl Pts',(-1.17817012667699,2.53688639776398,15.4703888888889));
#71191=CARTESIAN_POINT('Ctrl Pts',(-2.23297482288527,1.11978691060522,15.5756296296296));
#71192=CARTESIAN_POINT('Ctrl Pts',(-2.34668236863854,0.343918483395395,
15.62825));
#71193=CARTESIAN_POINT('',(-0.439445221994505,2.33068358199182,15.62825));
#71194=CARTESIAN_POINT('Origin',(0.,0.,15.62825));
#71195=CARTESIAN_POINT('Ctrl Pts',(-2.37517539399571,0.000929234209626874,
14.848589891905));
#71196=CARTESIAN_POINT('Ctrl Pts',(-2.37154287511732,-0.72977569986937,
14.8978167399366));
#71197=CARTESIAN_POINT('Ctrl Pts',(-1.620069408967,-2.24871933567263,14.9997085516349));
#71198=CARTESIAN_POINT('Ctrl Pts',(0.958368222991996,-2.62865236842956,
15.1542653269999));
#71199=CARTESIAN_POINT('Ctrl Pts',(2.7277014223945,-0.634378452891388,15.3122602179999));
#71200=CARTESIAN_POINT('Ctrl Pts',(2.01676643438217,1.93930517753648,15.470255109));
#71201=CARTESIAN_POINT('Ctrl Pts',(0.331786659212352,2.47609764328476,15.5755850363333));
#71202=CARTESIAN_POINT('Ctrl Pts',(-0.439445221994538,2.33068358199181,
15.62825));
#71203=CARTESIAN_POINT('Origin',(0.,0.,-1.84858989190501));
#71204=CARTESIAN_POINT('',(-2.36799142649297,0.000285102424211894,13.651410108095));
#71205=CARTESIAN_POINT('',(-2.37103403261776,-0.00209189776527924,13.848589891905));
#71206=CARTESIAN_POINT('',(-2.37175,-2.62313128856983E-13,-1.84858989190501));
#71207=CARTESIAN_POINT('Ctrl Pts',(-2.36799142649297,0.000285102424211897,
13.651410108095));
#71208=CARTESIAN_POINT('Ctrl Pts',(-2.36754527731231,-0.41108402173757,
13.6789122942855));
#71209=CARTESIAN_POINT('Ctrl Pts',(-2.07052456040773,-1.61013525385437,
13.7590348508465));
#71210=CARTESIAN_POINT('Ctrl Pts',(-0.16923542984156,-2.79279215602584,
13.8917777777778));
#71211=CARTESIAN_POINT('Ctrl Pts',(2.24512421134353,-1.66965318578134,14.0496388888889));
#71212=CARTESIAN_POINT('Ctrl Pts',(2.62593313585052,0.965751391486786,14.2075));
#71213=CARTESIAN_POINT('Ctrl Pts',(0.628359679142483,2.72647005025058,14.3653611111111));
#71214=CARTESIAN_POINT('Ctrl Pts',(-1.77762972544941,2.06202090562868,14.5133311471428));
#71215=CARTESIAN_POINT('Ctrl Pts',(-2.36707578383325,0.633891398858792,
14.6086808128041));
#71216=CARTESIAN_POINT('Ctrl Pts',(-2.37275986033066,-0.00196044888638126,
14.651410108095));
#71217=CARTESIAN_POINT('Ctrl Pts',(-2.37103403261776,-0.00209189776527889,
13.848589891905));
#71218=CARTESIAN_POINT('Ctrl Pts',(-2.37284080801943,-0.20941258958213,
13.8624953276032));
#71219=CARTESIAN_POINT('Ctrl Pts',(-2.25333213139831,-1.19988405133594,
13.929065726968));
#71220=CARTESIAN_POINT('Ctrl Pts',(-0.869666078203209,-2.66015561356989,
14.0483010899995));
#71221=CARTESIAN_POINT('Ctrl Pts',(1.75267763866885,-2.18191305067097,14.2062959809995));
#71222=CARTESIAN_POINT('Ctrl Pts',(2.78512620401791,0.275629071355557,14.3642908719996));
#71223=CARTESIAN_POINT('Ctrl Pts',(1.29091271455523,2.48320730756548,14.5222857629997));
#71224=CARTESIAN_POINT('Ctrl Pts',(-1.37414448785656,2.43798182357128,14.6802806539997));
#71225=CARTESIAN_POINT('Ctrl Pts',(-2.35095938458833,0.884486526760038,
14.7890486969682));
#71226=CARTESIAN_POINT('Ctrl Pts',(-2.37542909742077,0.0519633377314283,
14.8451517762699));
#71227=CARTESIAN_POINT('Ctrl Pts',(-2.37517539399571,0.000929234209626874,
14.848589891905));
#71228=CARTESIAN_POINT('Origin',(0.,0.,-1.84858989190501));
#71229=CARTESIAN_POINT('',(-2.3737947408518,0.00170749448784205,12.651410108095));
#71230=CARTESIAN_POINT('',(-2.36848474137664,0.00112338963946246,12.848589891905));
#71231=CARTESIAN_POINT('',(-2.37175,-2.62313128856983E-13,-1.84858989190501));
#71232=CARTESIAN_POINT('Ctrl Pts',(-2.3737947408518,0.00170749448784207,
12.651410108095));
#71233=CARTESIAN_POINT('Ctrl Pts',(-2.36833312974404,-0.668887685031927,
12.6965234053967));
#71234=CARTESIAN_POINT('Ctrl Pts',(-1.72235411599047,-2.13088047848934,
12.7942570730687));
#71235=CARTESIAN_POINT('Ctrl Pts',(0.750172845833004,-2.69546828972993,
12.9446111111111));
#71236=CARTESIAN_POINT('Ctrl Pts',(2.66668266040929,-0.846825037914988,
13.1024722222222));
#71237=CARTESIAN_POINT('Ctrl Pts',(2.16784415239069,1.76882949166842,13.2603333333333));
#71238=CARTESIAN_POINT('Ctrl Pts',(-0.294517949969841,2.78236767093066,
13.4181944444444));
#71239=CARTESIAN_POINT('Ctrl Pts',(-2.10760963637491,1.5382497642797,13.548553369365));
#71240=CARTESIAN_POINT('Ctrl Pts',(-2.36839890163746,0.375995067988055,
13.6262919239152));
#71241=CARTESIAN_POINT('Ctrl Pts',(-2.36799142649297,0.000285102424211897,
13.651410108095));
#71242=CARTESIAN_POINT('Ctrl Pts',(-2.36848474137664,0.00112338963946246,
12.848589891905));
#71243=CARTESIAN_POINT('Ctrl Pts',(-2.36646442019019,-0.466045225337024,
12.8798388789364));
#71244=CARTESIAN_POINT('Ctrl Pts',(-2.00748312661735,-1.72341304420753,
12.9637528296344));
#71245=CARTESIAN_POINT('Ctrl Pts',(0.0306296239850783,-2.7985342282319,
13.1003317439992));
#71246=CARTESIAN_POINT('Ctrl Pts',(2.36053793034993,-1.50352574600393,13.2583266349992));
#71247=CARTESIAN_POINT('Ctrl Pts',(2.54906768788899,1.15541663986578,13.4163215259993));
#71248=CARTESIAN_POINT('Ctrl Pts',(0.42518914129335,2.76621565710669,13.5743164169993));
#71249=CARTESIAN_POINT('Ctrl Pts',(-1.86352481270074,1.94670562977947,13.7184058723013));
#71250=CARTESIAN_POINT('Ctrl Pts',(-2.36599788968529,0.57578658999839,13.8098303639365));
#71251=CARTESIAN_POINT('Ctrl Pts',(-2.37103403261776,-0.00209189776527889,
13.848589891905));
#71252=CARTESIAN_POINT('Origin',(0.,0.,-1.84858989190501));
#71253=CARTESIAN_POINT('',(-2.37270243253876,-0.00200498951788303,11.651410108095));
#71254=CARTESIAN_POINT('',(-2.37496958658182,0.00104863022067879,11.848589891905));
#71255=CARTESIAN_POINT('',(-2.37175,-2.62313128856983E-13,-1.84858989190501));
#71256=CARTESIAN_POINT('Ctrl Pts',(-2.37270243253876,-0.00200498951788284,
11.651410108095));
#71257=CARTESIAN_POINT('Ctrl Pts',(-2.37405198430164,-0.152377883745359,
11.6615141461374));
#71258=CARTESIAN_POINT('Ctrl Pts',(-2.29281607417404,-1.08441874324097,
11.7242385545502));
#71259=CARTESIAN_POINT('Ctrl Pts',(-1.05977053720295,-2.58943908287633,
11.8395833333333));
#71260=CARTESIAN_POINT('Ctrl Pts',(1.58766534266525,-2.30382879610199,11.9974444444444));
#71261=CARTESIAN_POINT('Ctrl Pts',(2.79707340746319,0.0684743370742143,
12.1553055555555));
#71262=CARTESIAN_POINT('Ctrl Pts',(1.47303233105958,2.37875683253439,12.3131666666667));
#71263=CARTESIAN_POINT('Ctrl Pts',(-1.18520769732058,2.53448043892505,12.4710277777778));
#71264=CARTESIAN_POINT('Ctrl Pts',(-2.31706196946124,1.00613052370996,12.5837755915872));
#71265=CARTESIAN_POINT('Ctrl Pts',(-2.37470357962243,0.113297808503467,
12.6439030350263));
#71266=CARTESIAN_POINT('Ctrl Pts',(-2.3737947408518,0.00170749448784207,
12.651410108095));
#71267=CARTESIAN_POINT('Ctrl Pts',(-2.37496958658182,0.00104863022067909,
11.848589891905));
#71268=CARTESIAN_POINT('Ctrl Pts',(-2.37095686672064,-0.72032558818314,
11.8971824302696));
#71269=CARTESIAN_POINT('Ctrl Pts',(-1.63667192852724,-2.23060698037937,
11.9984399323009));
#71270=CARTESIAN_POINT('Ctrl Pts',(0.927689321261817,-2.64047796075702,
12.1523623979988));
#71271=CARTESIAN_POINT('Ctrl Pts',(2.71833714731268,-0.66586366962402,12.3103572889989));
#71272=CARTESIAN_POINT('Ctrl Pts',(2.04302496870488,1.91279385105346,12.468352179999));
#71273=CARTESIAN_POINT('Ctrl Pts',(-0.48563275555883,2.75624604578475,12.626347070999));
#71274=CARTESIAN_POINT('Ctrl Pts',(-2.16074812800628,1.4270578867686,12.7530929749677));
#71275=CARTESIAN_POINT('Ctrl Pts',(-2.36986933510064,0.32128967640745,12.8271739152697));
#71276=CARTESIAN_POINT('Ctrl Pts',(-2.36848474137664,0.00112338963946246,
12.848589891905));
#71277=CARTESIAN_POINT('Origin',(0.,0.,-1.84858989190501));
#71278=CARTESIAN_POINT('',(-2.3680043592011,0.000335278925106314,10.651410108095));
#71279=CARTESIAN_POINT('',(-2.37130727717011,-0.00210928510120167,10.848589891905));
#71280=CARTESIAN_POINT('',(-2.37175,-2.62313128856983E-13,-1.84858989190501));
#71281=CARTESIAN_POINT('Ctrl Pts',(-2.3680043592011,0.000335278925106194,
10.651410108095));
#71282=CARTESIAN_POINT('Ctrl Pts',(-2.36747521485208,-0.414214015593381,
10.6791252572485));
#71283=CARTESIAN_POINT('Ctrl Pts',(-2.06710351553143,-1.61654972761244,
10.7594607767724));
#71284=CARTESIAN_POINT('Ctrl Pts',(-0.158018739337926,-2.79344562132492,
10.8924166666667));
#71285=CARTESIAN_POINT('Ctrl Pts',(2.25180017160661,-1.66063371893121,11.0502777777778));
#71286=CARTESIAN_POINT('Ctrl Pts',(2.62205116590109,0.976297109112734,11.2081388888889));
#71287=CARTESIAN_POINT('Ctrl Pts',(0.617379419647229,2.72894686881467,11.366));
#71288=CARTESIAN_POINT('Ctrl Pts',(-1.78238141625357,2.05587933285381,11.5137570730687));
#71289=CARTESIAN_POINT('Ctrl Pts',(-2.36702371369352,0.630742424660346,
11.608893775767));
#71290=CARTESIAN_POINT('Ctrl Pts',(-2.37270243253876,-0.00200498951788284,
11.651410108095));
#71291=CARTESIAN_POINT('Ctrl Pts',(-2.37130727717011,-0.00210928510120129,
10.848589891905));
#71292=CARTESIAN_POINT('Ctrl Pts',(-2.37306236960384,-0.199914469168129,
10.8618610179362));
#71293=CARTESIAN_POINT('Ctrl Pts',(-2.26024839139859,-1.18071373741556,
10.927797107634));
#71294=CARTESIAN_POINT('Ctrl Pts',(-0.90141796228012,-2.64956165719617,
11.0463981609985));
#71295=CARTESIAN_POINT('Ctrl Pts',(1.72648179491819,-2.20272375262492,11.2043930519985));
#71296=CARTESIAN_POINT('Ctrl Pts',(2.7881905800153,0.242331605070017,11.3623879429986));
#71297=CARTESIAN_POINT('Ctrl Pts',(1.32057126786748,2.46755402056041,11.5203828339987));
#71298=CARTESIAN_POINT('Ctrl Pts',(-1.34501422335496,2.45431621031658,11.6783777249987));
#71299=CARTESIAN_POINT('Ctrl Pts',(-2.34590203170026,0.903460530701682,
11.7877800776342));
#71300=CARTESIAN_POINT('Ctrl Pts',(-2.37530588310888,0.0615052912262518,
11.8445174666029));
#71301=CARTESIAN_POINT('Ctrl Pts',(-2.37496958658182,0.00104863022067909,
11.848589891905));
#71302=CARTESIAN_POINT('Origin',(0.,0.,-1.84858989190501));
#71303=CARTESIAN_POINT('',(-2.37387835550442,0.0016747535505271,9.65141010809499));
#71304=CARTESIAN_POINT('',(-2.36835645684558,0.000990747813277848,9.84858989190503));
#71305=CARTESIAN_POINT('',(-2.37175,-2.62313128856983E-13,-1.84858989190501));
#71306=CARTESIAN_POINT('Ctrl Pts',(-2.37387835550442,0.00167475355052717,
9.65141010809499));
#71307=CARTESIAN_POINT('Ctrl Pts',(-2.36846517734921,-0.672024104003181,
9.69673636835963));
#71308=CARTESIAN_POINT('Ctrl Pts',(-1.71729169385484,-2.1369916722257,9.79468299899462));
#71309=CARTESIAN_POINT('Ctrl Pts',(0.760987165659879,-2.69243512365168,
9.94525));
#71310=CARTESIAN_POINT('Ctrl Pts',(2.6700603672968,-0.836113626465368,10.1031111111111));
#71311=CARTESIAN_POINT('Ctrl Pts',(2.16072649637127,1.7775177549783,10.2609722222222));
#71312=CARTESIAN_POINT('Ctrl Pts',(-0.305685313585232,2.78116249982291,
10.4188333333333));
#71313=CARTESIAN_POINT('Ctrl Pts',(-2.11081288774265,1.53182193243431,10.5489792952909));
#71314=CARTESIAN_POINT('Ctrl Pts',(-2.36847985572451,0.37285508129321,10.6265048868781));
#71315=CARTESIAN_POINT('Ctrl Pts',(-2.3680043592011,0.000335278925106194,
10.651410108095));
#71316=CARTESIAN_POINT('Ctrl Pts',(-2.36835645684558,0.00099074781327764,
9.84858989190503));
#71317=CARTESIAN_POINT('Ctrl Pts',(-2.36661646666674,-0.456757128880904,
9.87920456926939));
#71318=CARTESIAN_POINT('Ctrl Pts',(-2.01853982608692,-1.70439405627733,
9.96248421030043));
#71319=CARTESIAN_POINT('Ctrl Pts',(-0.00283249851198579,-2.79870028674429,
10.0984288149982));
#71320=CARTESIAN_POINT('Ctrl Pts',(2.34239313895008,-1.53164150527581,10.2564237059982));
#71321=CARTESIAN_POINT('Ctrl Pts',(2.56269918704329,1.12485741087042,10.4144185969983));
#71322=CARTESIAN_POINT('Ctrl Pts',(0.458233353927178,2.76093344928963,10.5724134879983));
#71323=CARTESIAN_POINT('Ctrl Pts',(-1.85023633825226,1.96536160231837,10.7171372529672));
#71324=CARTESIAN_POINT('Ctrl Pts',(-2.36609748365237,0.585053046589831,
10.8091960542695));
#71325=CARTESIAN_POINT('Ctrl Pts',(-2.37130727717011,-0.00210928510120129,
10.848589891905));
#71326=CARTESIAN_POINT('Origin',(0.,0.,-1.84858989190501));
#71327=CARTESIAN_POINT('',(-2.37260887298938,-0.00202072084187682,8.65141010809499));
#71328=CARTESIAN_POINT('',(-2.3747901511292,0.00119133359606532,8.84858989190503));
#71329=CARTESIAN_POINT('',(-2.37175,-2.62313128856983E-13,-1.84858989190501));
#71330=CARTESIAN_POINT('Ctrl Pts',(-2.37260887298937,-0.00202072084187674,
8.65141010809499));
#71331=CARTESIAN_POINT('Ctrl Pts',(-2.37399141457934,-0.155578652695773,
8.66172710910036));
#71332=CARTESIAN_POINT('Ctrl Pts',(-2.29073220490892,-1.09084435213441,
8.72466448047611));
#71333=CARTESIAN_POINT('Ctrl Pts',(-1.04936735270146,-2.59367240037321,
8.84022222222223));
#71334=CARTESIAN_POINT('Ctrl Pts',(1.59690068918271,-2.29743695240177,8.99808333333332));
#71335=CARTESIAN_POINT('Ctrl Pts',(2.79677599470576,0.0797019247629725,
9.15594444444445));
#71336=CARTESIAN_POINT('Ctrl Pts',(1.46347155312646,2.38465078671139,9.31380555555555));
#71337=CARTESIAN_POINT('Ctrl Pts',(-1.19537219008389,2.52970229247383,9.47166666666666));
#71338=CARTESIAN_POINT('Ctrl Pts',(-2.31895585283185,0.999716542450464,
9.58420151751315));
#71339=CARTESIAN_POINT('Ctrl Pts',(-2.37474946901026,0.110089469797055,
9.64411599798926));
#71340=CARTESIAN_POINT('Ctrl Pts',(-2.37387835550442,0.00167475355052717,
9.65141010809499));
#71341=CARTESIAN_POINT('Ctrl Pts',(-2.3747901511292,0.00119133359606537,
8.84858989190503));
#71342=CARTESIAN_POINT('Ctrl Pts',(-2.37038906205444,-0.71090872088079,
8.89654812060261));
#71343=CARTESIAN_POINT('Ctrl Pts',(-1.65267775677864,-2.21269450774448,
8.99717131296688));
#71344=CARTESIAN_POINT('Ctrl Pts',(0.896053003445084,-2.6513808351669,9.15045946899784));
#71345=CARTESIAN_POINT('Ctrl Pts',(2.71018167460651,-0.698316982967359,
9.30845435999788));
#71346=CARTESIAN_POINT('Ctrl Pts',(2.06574861445826,1.88823038317285,9.46644925099794));
#71347=CARTESIAN_POINT('Ctrl Pts',(-0.45264386973844,2.76185532663481,9.62444414199799));
#71348=CARTESIAN_POINT('Ctrl Pts',(-2.15199374797492,1.44623886325989,9.75182435563369));
#71349=CARTESIAN_POINT('Ctrl Pts',(-2.36960968846224,0.330684626839437,
9.8265396056027));
#71350=CARTESIAN_POINT('Ctrl Pts',(-2.36835645684558,0.00099074781327764,
9.84858989190503));
#71351=CARTESIAN_POINT('Origin',(0.,0.,-1.84858989190501));
#71352=CARTESIAN_POINT('',(-2.36801892187683,0.000385579322849399,7.65141010809499));
#71353=CARTESIAN_POINT('',(-2.37158591103805,-0.00211396583053219,7.84858989190503));
#71354=CARTESIAN_POINT('',(-2.37175,-2.62313128856983E-13,-1.84858989190501));
#71355=CARTESIAN_POINT('Ctrl Pts',(-2.36801892187683,0.000385579322849869,
7.65141010809499));
#71356=CARTESIAN_POINT('Ctrl Pts',(-2.36740549965901,-0.417342685994756,
7.67933822021147));
#71357=CARTESIAN_POINT('Ctrl Pts',(-2.06366306314178,-1.62296175556451,
7.75988670269832));
#71358=CARTESIAN_POINT('Ctrl Pts',(-0.146803886877873,-2.79405744038503,
7.89305555555557));
#71359=CARTESIAN_POINT('Ctrl Pts',(2.25844822171206,-1.65158105802259,8.05091666666665));
#71360=CARTESIAN_POINT('Ctrl Pts',(2.61811094239596,0.986814802625037,8.20877777777778));
#71361=CARTESIAN_POINT('Ctrl Pts',(0.606419780073446,2.73140319464357,8.36663888888888));
#71362=CARTESIAN_POINT('Ctrl Pts',(-1.7871649975578,2.04969182184781,8.51418299899463));
#71363=CARTESIAN_POINT('Ctrl Pts',(-2.36693996130543,0.627621353124904,
8.60910673873));
#71364=CARTESIAN_POINT('Ctrl Pts',(-2.37260887298937,-0.00202072084187674,
8.65141010809499));
#71365=CARTESIAN_POINT('Ctrl Pts',(-2.37158591103805,-0.002113965830532,
7.84858989190503));
#71366=CARTESIAN_POINT('Ctrl Pts',(-2.37327853101496,-0.190408271679788,
7.86122670826915));
#71367=CARTESIAN_POINT('Ctrl Pts',(-2.26703071089283,-1.16154754141212,
7.92652848829996));
#71368=CARTESIAN_POINT('Ctrl Pts',(-0.9330321424437,-2.63859476601473,8.04449523199746));
#71369=CARTESIAN_POINT('Ctrl Pts',(1.70002224901497,-2.22320841823872,8.2024901229975));
#71370=CARTESIAN_POINT('Ctrl Pts',(2.79088864512093,0.208978201275766,8.36048501399757));
#71371=CARTESIAN_POINT('Ctrl Pts',(1.34997937336987,2.45158867054595,8.51847990499762));
#71372=CARTESIAN_POINT('Ctrl Pts',(-1.31557386100644,2.47022200101732,8.67647479599767));
#71373=CARTESIAN_POINT('Ctrl Pts',(-2.34084261733164,0.922522196646213,
8.78651145830014));
#71374=CARTESIAN_POINT('Ctrl Pts',(-2.37522208450983,0.0710785316625285,
8.84388315693593));
#71375=CARTESIAN_POINT('Ctrl Pts',(-2.3747901511292,0.00119133359606537,
8.84858989190503));
#71376=CARTESIAN_POINT('Origin',(0.,0.,-1.84858989190501));
#71377=CARTESIAN_POINT('',(-2.37396076251026,0.0016408096299993,6.65141010809499));
#71378=CARTESIAN_POINT('',(-2.36824488832617,0.00085307042009708,6.84858989190503));
#71379=CARTESIAN_POINT('',(-2.37175,-2.62313128856983E-13,-1.84858989190501));
#71380=CARTESIAN_POINT('Ctrl Pts',(-2.37396076251026,0.00164080962999946,
6.65141010809499));
#71381=CARTESIAN_POINT('Ctrl Pts',(-2.36860111288507,-0.675161988858878,
6.69694933132258));
#71382=CARTESIAN_POINT('Ctrl Pts',(-1.71220786555833,-2.14309654094568,
6.79510892492056));
#71383=CARTESIAN_POINT('Ctrl Pts',(0.771789132562049,-2.68935864031417,
6.94588888888888));
#71384=CARTESIAN_POINT('Ctrl Pts',(2.67339522049833,-0.825388609316905,
7.10375));
#71385=CARTESIAN_POINT('Ctrl Pts',(2.15357369271338,1.7861771220756,7.26161111111111));
#71386=CARTESIAN_POINT('Ctrl Pts',(-0.3168471224657,2.77991299546561,7.41947222222222));
#71387=CARTESIAN_POINT('Ctrl Pts',(-2.11399942046796,1.52539245310181,7.54940522121685));
#71388=CARTESIAN_POINT('Ctrl Pts',(-2.36856127073871,0.369714310321545,
7.62671784984111));
#71389=CARTESIAN_POINT('Ctrl Pts',(-2.36801892187683,0.000385579322849869,
7.65141010809499));
#71390=CARTESIAN_POINT('Ctrl Pts',(-2.36824488832617,0.000853070420097184,
6.84858989190503));
#71391=CARTESIAN_POINT('Ctrl Pts',(-2.36678180876479,-0.447463537758943,
6.87857025960238));
#71392=CARTESIAN_POINT('Ctrl Pts',(-2.02943011823198,-1.68535627820218,
6.96121559096642));
#71393=CARTESIAN_POINT('Ctrl Pts',(-0.0362940343214689,-2.79846637663312,
7.09652588599712));
#71394=CARTESIAN_POINT('Ctrl Pts',(2.32391314315961,-1.55953807940794,7.2545207769972));
#71395=CARTESIAN_POINT('Ctrl Pts',(2.57596499873257,1.09413693995685,7.41251566799723));
#71396=CARTESIAN_POINT('Ctrl Pts',(0.491210792034311,2.75525738831465,7.5705105589973));
#71397=CARTESIAN_POINT('Ctrl Pts',(-1.83676464589149,1.98397717256952,7.71586863363322));
#71398=CARTESIAN_POINT('Ctrl Pts',(-2.36622439910258,0.594323617306658,
7.80856174460247));
#71399=CARTESIAN_POINT('Ctrl Pts',(-2.37158591103805,-0.002113965830532,
7.84858989190503));
#71400=CARTESIAN_POINT('Origin',(0.,0.,-1.84858989190501));
#71401=CARTESIAN_POINT('',(-2.37251499866524,-0.00203510706959473,5.65141010809499));
#71402=CARTESIAN_POINT('',(-2.37459246787895,0.00132584644941116,5.84858989190502));
#71403=CARTESIAN_POINT('',(-2.37175,-2.62313128856983E-13,-1.84858989190501));
#71404=CARTESIAN_POINT('Ctrl Pts',(-2.37251499866524,-0.00203510706959476,
5.65141010809499));
#71405=CARTESIAN_POINT('Ctrl Pts',(-2.37392982983489,-0.158778764602934,
5.66194007206332));
#71406=CARTESIAN_POINT('Ctrl Pts',(-2.28863365792017,-1.09727074999648,
5.72509040640203));
#71407=CARTESIAN_POINT('Ctrl Pts',(-1.03894725747156,-2.59786392206505,
5.84086111111111));
#71408=CARTESIAN_POINT('Ctrl Pts',(1.60611030100396,-2.29100808867664,5.99872222222222));
#71409=CARTESIAN_POINT('Ctrl Pts',(2.79643351757374,0.090928230838667,6.15658333333333));
#71410=CARTESIAN_POINT('Ctrl Pts',(1.45388718569001,2.39050630885174,6.31444444444444));
#71411=CARTESIAN_POINT('Ctrl Pts',(-1.20551740739643,2.52488339173069,6.47230555555556));
#71412=CARTESIAN_POINT('Ctrl Pts',(-2.3208356274226,0.99330351170231,6.58462744343907));
#71413=CARTESIAN_POINT('Ctrl Pts',(-2.37479416424485,0.106880641648857,
6.64432896095221));
#71414=CARTESIAN_POINT('Ctrl Pts',(-2.37396076251026,0.00164080962999946,
6.65141010809499));
#71415=CARTESIAN_POINT('Ctrl Pts',(-2.37459246787895,0.00132584644941126,
5.84858989190502));
#71416=CARTESIAN_POINT('Ctrl Pts',(-2.3698592307678,-0.701510136856058,
5.8959138109356));
#71417=CARTESIAN_POINT('Ctrl Pts',(-1.6684907359976,-2.19471791424095,5.99590269363287));
#71418=CARTESIAN_POINT('Ctrl Pts',(0.864288593995119,-2.66190468356086,
6.14855653999681));
#71419=CARTESIAN_POINT('Ctrl Pts',(2.70163876039796,-0.730670463607777,
6.30655143099686));
#71420=CARTESIAN_POINT('Ctrl Pts',(2.08817696449889,1.86339697407977,6.46454632199692));
#71421=CARTESIAN_POINT('Ctrl Pts',(-0.419590302218696,2.76706980330411,
6.62254121299697));
#71422=CARTESIAN_POINT('Ctrl Pts',(-2.14308835195883,1.46541542002878,6.75055573629967));
#71423=CARTESIAN_POINT('Ctrl Pts',(-2.36935192507288,0.340071095547311,
6.82590529593569));
#71424=CARTESIAN_POINT('Ctrl Pts',(-2.36824488832617,0.000853070420097184,
6.84858989190503));
#71425=CARTESIAN_POINT('Origin',(0.,0.,-1.84858989190501));
#71426=CARTESIAN_POINT('',(-2.36803551809634,0.000435659979227324,4.65141010809499));
#71427=CARTESIAN_POINT('',(-2.37186713520955,-0.00210673407030348,4.84858989190502));
#71428=CARTESIAN_POINT('',(-2.37175,-2.62313128856983E-13,-1.84858989190501));
#71429=CARTESIAN_POINT('Ctrl Pts',(-2.36803551809634,0.000435659979227676,
4.65141010809499));
#71430=CARTESIAN_POINT('Ctrl Pts',(-2.36733685507668,-0.420470574046625,
4.67955118317444));
#71431=CARTESIAN_POINT('Ctrl Pts',(-2.06020439223756,-1.62937224150312,
4.76031262862425));
#71432=CARTESIAN_POINT('Ctrl Pts',(-0.135586668767159,-2.79462423533096,
4.89369444444444));
#71433=CARTESIAN_POINT('Ctrl Pts',(2.2650598786042,-1.64250178316317,5.05155555555556));
#71434=CARTESIAN_POINT('Ctrl Pts',(2.61412853009539,0.997316594419356,5.20941666666666));
#71435=CARTESIAN_POINT('Ctrl Pts',(0.595450368366912,2.73381550588105,5.36727777777778));
#71436=CARTESIAN_POINT('Ctrl Pts',(-1.79192767962886,2.0434990191552,5.51460892492054));
#71437=CARTESIAN_POINT('Ctrl Pts',(-2.36685963088812,0.624501153297232,
5.60931970169295));
#71438=CARTESIAN_POINT('Ctrl Pts',(-2.37251499866524,-0.00203510706959476,
5.65141010809499));
#71439=CARTESIAN_POINT('Ctrl Pts',(-2.37186713520955,-0.00210673407030307,
4.84858989190502));
#71440=CARTESIAN_POINT('Ctrl Pts',(-2.37348726775032,-0.180895246540068,
4.86059239860214));
#71441=CARTESIAN_POINT('Ctrl Pts',(-2.27367886126175,-1.14238681798702,
4.92525986896595));
#71442=CARTESIAN_POINT('Ctrl Pts',(-0.964512940920624,-2.62725067416123,
5.04259230299644));
#71443=CARTESIAN_POINT('Ctrl Pts',(1.67331967629405,-2.24337526486265,5.20058719399648));
#71444=CARTESIAN_POINT('Ctrl Pts',(2.79318773824162,0.175594923072764,5.35858208499656));
#71445=CARTESIAN_POINT('Ctrl Pts',(1.37919449268132,2.43527285317938,5.51657697599659));
#71446=CARTESIAN_POINT('Ctrl Pts',(-1.28594543116668,2.48577466117395,5.67457186699666));
#71447=CARTESIAN_POINT('Ctrl Pts',(-2.33566190719347,0.94159330950118,5.78524283896613));
#71448=CARTESIAN_POINT('Ctrl Pts',(-2.37512666773395,0.0806489125773547,
5.84324884726892));
#71449=CARTESIAN_POINT('Ctrl Pts',(-2.37459246787895,0.00132584644941126,
5.84858989190502));
#71450=CARTESIAN_POINT('Origin',(0.,0.,-1.84858989190501));
#71451=CARTESIAN_POINT('',(-2.37404189208837,0.00160568163382189,3.65141010809499));
#71452=CARTESIAN_POINT('',(-2.36815046112586,0.00071106261527204,3.84858989190502));
#71453=CARTESIAN_POINT('',(-2.37175,-2.62313128856983E-13,-1.84858989190501));
#71454=CARTESIAN_POINT('Ctrl Pts',(-2.37404189208837,0.0016056816338219,
3.65141010809499));
#71455=CARTESIAN_POINT('Ctrl Pts',(-2.36874097406567,-0.678301390146093,
3.69716229428555));
#71456=CARTESIAN_POINT('Ctrl Pts',(-1.70710264047504,-2.14919504149034,
3.79553485084648));
#71457=CARTESIAN_POINT('Ctrl Pts',(0.782578662553965,-2.68623882063674,
3.94652777777777));
#71458=CARTESIAN_POINT('Ctrl Pts',(2.67668699402767,-0.814650291328897,
4.10438888888889));
#71459=CARTESIAN_POINT('Ctrl Pts',(2.14638618582228,1.79480770611467,4.26225));
#71460=CARTESIAN_POINT('Ctrl Pts',(-0.328003825581952,2.77861869501174,
4.42011111111111));
#71461=CARTESIAN_POINT('Ctrl Pts',(-2.1171683957745,1.51896204170615,4.54983114714277));
#71462=CARTESIAN_POINT('Ctrl Pts',(-2.3686432695173,0.366572631058683,4.62693081280407));
#71463=CARTESIAN_POINT('Ctrl Pts',(-2.36803551809634,0.000435659979227676,
4.65141010809499));
#71464=CARTESIAN_POINT('Ctrl Pts',(-2.36815046112586,0.000711062615271901,
3.84858989190502));
#71465=CARTESIAN_POINT('Ctrl Pts',(-2.36695951468436,-0.438164069114789,
3.87793594993537));
#71466=CARTESIAN_POINT('Ctrl Pts',(-2.04015506879268,-1.66630099353556,
3.9599469716324));
#71467=CARTESIAN_POINT('Ctrl Pts',(-0.0697503817448946,-2.79783241149437,
4.09462295699612));
#71468=CARTESIAN_POINT('Ctrl Pts',(2.30510093209087,-1.58721170953314,4.25261784799616));
#71469=CARTESIAN_POINT('Ctrl Pts',(2.5888625630092,1.06326005653742,4.41061273899623));
#71470=CARTESIAN_POINT('Ctrl Pts',(0.524118009051023,2.74918744918107,4.56860762999628));
#71471=CARTESIAN_POINT('Ctrl Pts',(-1.82311086019465,2.00255204277458,4.71460001429921));
#71472=CARTESIAN_POINT('Ctrl Pts',(-2.36637840094874,0.603598422228309,
4.80792743493546));
#71473=CARTESIAN_POINT('Ctrl Pts',(-2.37186713520955,-0.00210673407030307,
4.84858989190502));
#71474=CARTESIAN_POINT('Origin',(0.,0.,-1.84858989190501));
#71475=CARTESIAN_POINT('',(-2.37242086931256,-0.00204814969984112,2.65141010809499));
#71476=CARTESIAN_POINT('',(-2.37437841508221,0.00145143062880153,2.84858989190502));
#71477=CARTESIAN_POINT('',(-2.37175,-2.62313128856983E-13,-1.84858989190501));
#71478=CARTESIAN_POINT('Ctrl Pts',(-2.37242086931256,-0.00204814969984169,
2.65141010809499));
#71479=CARTESIAN_POINT('Ctrl Pts',(-2.37386724785776,-0.161978223542019,
2.66215303502629));
#71480=CARTESIAN_POINT('Ctrl Pts',(-2.28652040521148,-1.10369798895945,
2.72551633232796));
#71481=CARTESIAN_POINT('Ctrl Pts',(-1.02851040967351,-2.60201352259292,
2.84149999999999));
#71482=CARTESIAN_POINT('Ctrl Pts',(1.61529402596567,-2.28454233775194,2.99936111111111));
#71483=CARTESIAN_POINT('Ctrl Pts',(2.79604598097933,0.102153087721166,3.15722222222222));
#71484=CARTESIAN_POINT('Ctrl Pts',(1.44427938842878,2.39632330140064,3.31508333333333));
#71485=CARTESIAN_POINT('Ctrl Pts',(-1.21564319790733,2.5200238088076,3.47294444444445));
#71486=CARTESIAN_POINT('Ctrl Pts',(-2.32270131739363,0.986891451715146,
3.58505336936499));
#71487=CARTESIAN_POINT('Ctrl Pts',(-2.37483765037521,0.103671339757588,
3.64454192391517));
#71488=CARTESIAN_POINT('Ctrl Pts',(-2.37404189208837,0.0016056816338219,
3.65141010809499));
#71489=CARTESIAN_POINT('Ctrl Pts',(-2.37437841508221,0.00145143062880148,
2.84858989190502));
#71490=CARTESIAN_POINT('Ctrl Pts',(-2.36936657242201,-0.69212851464997,
2.89527950126859));
#71491=CARTESIAN_POINT('Ctrl Pts',(-1.68411161328175,-2.17667922631145,
2.99463407429885));
#71492=CARTESIAN_POINT('Ctrl Pts',(0.832400628534772,-2.67204800324426,
3.1466536109958));
#71493=CARTESIAN_POINT('Ctrl Pts',(2.69270963387839,-0.762919488957052,
3.30464850199585));
#71494=CARTESIAN_POINT('Ctrl Pts',(2.11030679852043,1.83829718168443,3.4626433929959));
#71495=CARTESIAN_POINT('Ctrl Pts',(-0.386476751895552,2.77188871376435,
3.62063828399595));
#71496=CARTESIAN_POINT('Ctrl Pts',(-2.13403081733917,1.48458669705641,3.74928711696566));
#71497=CARTESIAN_POINT('Ctrl Pts',(-2.36909680859298,0.349449137499666,
3.82527098626868));
#71498=CARTESIAN_POINT('Ctrl Pts',(-2.36815046112586,0.000711062615271901,
3.84858989190502));
#71499=CARTESIAN_POINT('Origin',(0.,0.,-1.84858989190501));
#71500=CARTESIAN_POINT('',(-2.36805372255214,0.000487775483918624,1.65141010809499));
#71501=CARTESIAN_POINT('',(-2.37214954248261,-0.00208751672060303,1.84858989190502));
#71502=CARTESIAN_POINT('',(-2.37175,-2.62313128856983E-13,-1.84858989190501));
#71503=CARTESIAN_POINT('Ctrl Pts',(-2.36805372255214,0.000487775483918769,
1.65141010809499));
#71504=CARTESIAN_POINT('Ctrl Pts',(-2.36726911244657,-0.423596588857836,
1.6797641461374));
#71505=CARTESIAN_POINT('Ctrl Pts',(-2.0567282222087,-1.63578530702029,1.76073855455018));
#71506=CARTESIAN_POINT('Ctrl Pts',(-0.124366744542119,-2.79514315034066,
1.89433333333333));
#71507=CARTESIAN_POINT('Ctrl Pts',(2.27163476293377,-1.63339753074864,2.05219444444444));
#71508=CARTESIAN_POINT('Ctrl Pts',(2.61010413592219,1.00780309522069,2.21005555555555));
#71509=CARTESIAN_POINT('Ctrl Pts',(0.584471286669745,2.73618335546233,2.36791666666667));
#71510=CARTESIAN_POINT('Ctrl Pts',(-1.79666946585791,2.03730116384381,2.51503485084647));
#71511=CARTESIAN_POINT('Ctrl Pts',(-2.36678268187025,0.621381820955435,
2.60953266465592));
#71512=CARTESIAN_POINT('Ctrl Pts',(-2.37242086931256,-0.00204814969984169,
2.65141010809499));
#71513=CARTESIAN_POINT('Ctrl Pts',(-2.37214954248261,-0.00208751672060286,
1.84858989190502));
#71514=CARTESIAN_POINT('Ctrl Pts',(-2.37368814589582,-0.171375740131997,
1.85995808893514));
#71515=CARTESIAN_POINT('Ctrl Pts',(-2.28019409230745,-1.12323247312203,
1.92399124963194));
#71516=CARTESIAN_POINT('Ctrl Pts',(-0.995855715555496,-2.61553061219188,
2.04068937399542));
#71517=CARTESIAN_POINT('Ctrl Pts',(1.64637781974439,-2.26322161422709,2.19868426499547));
#71518=CARTESIAN_POINT('Ctrl Pts',(2.79508756969503,0.142186649832604,2.35667915599553));
#71519=CARTESIAN_POINT('Ctrl Pts',(1.40821242874264,2.41860884498944,2.51467404699558));
#71520=CARTESIAN_POINT('Ctrl Pts',(-1.25613315819632,2.50097199645567,2.67266893799564));
#71521=CARTESIAN_POINT('Ctrl Pts',(-2.33035893824447,0.960673681793537,
2.78397421963211));
#71522=CARTESIAN_POINT('Ctrl Pts',(-2.37501983264844,0.0902160608552179,
2.84261453760191));
#71523=CARTESIAN_POINT('Ctrl Pts',(-2.37437841508221,0.00145143062880148,
2.84858989190502));
#71524=CARTESIAN_POINT('Origin',(0.,0.,-1.84858989190501));
#71525=CARTESIAN_POINT('',(-2.37409249406917,0.00172857025301859,0.651410108094985));
#71526=CARTESIAN_POINT('',(-2.36806791026422,0.000580996437929415,0.848589891905023));
#71527=CARTESIAN_POINT('',(-2.37175,-2.62313128856983E-13,-1.84858989190501));
#71528=CARTESIAN_POINT('Ctrl Pts',(-2.37409249406917,0.00172857025301858,
0.651410108094986));
#71529=CARTESIAN_POINT('Ctrl Pts',(-2.36885059157359,-0.681255271864669,
0.697375257248508));
#71530=CARTESIAN_POINT('Ctrl Pts',(-1.70202128243095,-2.15553453151225,
0.7959607767724));
#71531=CARTESIAN_POINT('Ctrl Pts',(0.793380919254056,-2.68293732976497,
0.947166666666663));
#71532=CARTESIAN_POINT('Ctrl Pts',(2.67992237177449,-0.803971281251394,
1.10502777777777));
#71533=CARTESIAN_POINT('Ctrl Pts',(2.13917103413275,1.80344728451176,1.26288888888888));
#71534=CARTESIAN_POINT('Ctrl Pts',(-0.339158877291603,2.77725977180218,
1.42075));
#71535=CARTESIAN_POINT('Ctrl Pts',(-2.12031894951391,1.51253569372851,1.5502570730687));
#71536=CARTESIAN_POINT('Ctrl Pts',(-2.36872521807391,0.363433332120877,
1.62714377576703));
#71537=CARTESIAN_POINT('Ctrl Pts',(-2.36805372255214,0.000487775483918769,
1.65141010809499));
#71538=CARTESIAN_POINT('Ctrl Pts',(-2.36806791026422,0.000580996437929554,
0.848589891905023));
#71539=CARTESIAN_POINT('Ctrl Pts',(-2.36714590954407,-0.428850691797627,
0.877301640268363));
#71540=CARTESIAN_POINT('Ctrl Pts',(-2.05072593975983,-1.64725737587436,
0.958678352298389));
#71541=CARTESIAN_POINT('Ctrl Pts',(-0.103189861818606,-2.79677945469355,
1.0927200279951));
#71542=CARTESIAN_POINT('Ctrl Pts',(2.28595558559378,-1.6146683983646,1.25071491899515));
#71543=CARTESIAN_POINT('Ctrl Pts',(2.60139192527736,1.0322363870214,1.4087098099952));
#71544=CARTESIAN_POINT('Ctrl Pts',(0.556949311928898,2.7427217714679,1.56670470099526));
#71545=CARTESIAN_POINT('Ctrl Pts',(-1.80927361374524,2.02108563130788,1.7133313949652));
#71546=CARTESIAN_POINT('Ctrl Pts',(-2.36656032319539,0.612878624174093,
1.80729312526845));
#71547=CARTESIAN_POINT('Ctrl Pts',(-2.37214954248261,-0.00208751672060286,
1.84858989190502));
#71548=CARTESIAN_POINT('Origin',(0.,0.,15.5));
#71549=CARTESIAN_POINT('',(-2.86987326377042,0.00104132824445593,15.1339652973708));
#71550=CARTESIAN_POINT('Ctrl Pts',(-0.439445221994174,2.33068358199188,
15.62825));
#71551=CARTESIAN_POINT('Ctrl Pts',(-0.359491362851287,2.34930954683752,
15.6247606402091));
#71552=CARTESIAN_POINT('Ctrl Pts',(-0.27873128971825,2.36341107797762,15.6212855109979));
#71553=CARTESIAN_POINT('Ctrl Pts',(-0.197490043658781,2.37317361481181,
15.6178198845782));
#71554=CARTESIAN_POINT('Ctrl Pts',(-0.114097433923979,2.38319467509491,
15.6142624842978));
#71555=CARTESIAN_POINT('Ctrl Pts',(-0.0301970746788968,2.38864392614809,
15.610715096763));
#71556=CARTESIAN_POINT('Ctrl Pts',(0.0538748377108959,2.38966967391038,
15.6071726085593));
#71557=CARTESIAN_POINT('Ctrl Pts',(0.0936167287327529,2.39015455827456,
15.6054980281181));
#71558=CARTESIAN_POINT('Ctrl Pts',(0.133397101437596,2.38965022998153,15.6038245424699));
#71559=CARTESIAN_POINT('Ctrl Pts',(0.17318082101162,2.38816842541213,15.6021516114778));
#71560=CARTESIAN_POINT('Ctrl Pts',(0.19744268730314,2.38726475565179,15.601131384398));
#71561=CARTESIAN_POINT('Ctrl Pts',(0.221705799792773,2.38599750448324,15.6001113636003));
#71562=CARTESIAN_POINT('Ctrl Pts',(0.245962166148401,2.38436888753973,15.5990914265778));
#71563=CARTESIAN_POINT('Ctrl Pts',(0.26185491634123,2.38330181913124,15.5984231647255));
#71564=CARTESIAN_POINT('Ctrl Pts',(0.277745619245824,2.38207945021967,15.597754902985));
#71565=CARTESIAN_POINT('Ctrl Pts',(0.293615508622687,2.38070402970992,15.5970873017022));
#71566=CARTESIAN_POINT('Ctrl Pts',(0.379355905904818,2.37327303267301,15.5934804461119));
#71567=CARTESIAN_POINT('Ctrl Pts',(0.46460122999168,2.36137220783444,15.5898881158652));
#71568=CARTESIAN_POINT('Ctrl Pts',(0.548999070996607,2.3451645872232,15.5863050764217));
#71569=CARTESIAN_POINT('Ctrl Pts',(0.634137600151781,2.32881472609505,15.582690591685));
#71570=CARTESIAN_POINT('Ctrl Pts',(0.718414656351904,2.30808199543454,15.5790855615419));
#71571=CARTESIAN_POINT('Ctrl Pts',(0.801467682213623,2.28308069981211,15.5754846124216));
#71572=CARTESIAN_POINT('Ctrl Pts',(0.852459500288906,2.26773072905791,15.573273748452));
#71573=CARTESIAN_POINT('Ctrl Pts',(0.902989840792886,2.2507706713731,15.5710644228464));
#71574=CARTESIAN_POINT('Ctrl Pts',(0.952972256247749,2.23221757070223,15.5688553919549));
#71575=CARTESIAN_POINT('Ctrl Pts',(0.964785636442244,2.22783253188374,15.5683332858993));
#71576=CARTESIAN_POINT('Ctrl Pts',(0.976567164733754,2.22335887755768,15.5678112499871));
#71577=CARTESIAN_POINT('Ctrl Pts',(0.98830665315667,2.21880049805757,15.5672896716409));
#71578=CARTESIAN_POINT('Ctrl Pts',(1.07009362440554,2.18704306198486,15.5636559261431));
#71579=CARTESIAN_POINT('Ctrl Pts',(1.14996182974845,2.15113305037133,15.5600390318413));
#71580=CARTESIAN_POINT('Ctrl Pts',(1.22755227573139,2.11121890826833,15.5564336755567));
#71581=CARTESIAN_POINT('Ctrl Pts',(1.30476387614222,2.07149965222131,15.552845922899));
#71582=CARTESIAN_POINT('Ctrl Pts',(1.37972085381243,2.02781498993708,15.5492695958616));
#71583=CARTESIAN_POINT('Ctrl Pts',(1.45205674723287,1.98026157738062,15.5456994587133));
#71584=CARTESIAN_POINT('Ctrl Pts',(1.51163119176407,1.94109750537355,15.5427591627211));
#71585=CARTESIAN_POINT('Ctrl Pts',(1.56942781249227,1.89930836286272,15.5398230652386));
#71586=CARTESIAN_POINT('Ctrl Pts',(1.62522850219512,1.85492460083693,15.5368882414682));
#71587=CARTESIAN_POINT('Ctrl Pts',(1.65312884704655,1.83273271982404,15.5354208295831));
#71588=CARTESIAN_POINT('Ctrl Pts',(1.68052998038672,1.80989186082895,15.5339537361259));
#71589=CARTESIAN_POINT('Ctrl Pts',(1.70740302888556,1.78640394209333,15.532486595497));
#71590=CARTESIAN_POINT('Ctrl Pts',(1.72592667853778,1.77021366960761,15.5314752923321));
#71591=CARTESIAN_POINT('Ctrl Pts',(1.74419939199006,1.753715928893,15.5304639667541));
#71592=CARTESIAN_POINT('Ctrl Pts',(1.76221135665739,1.73691101229318,15.5294524990243));
#71593=CARTESIAN_POINT('Ctrl Pts',(1.77033011726031,1.72933631972932,15.528996587384));
#71594=CARTESIAN_POINT('Ctrl Pts',(1.77839409985328,1.72170084478485,15.5285407465195));
#71595=CARTESIAN_POINT('Ctrl Pts',(1.78639747681482,1.71400960641012,15.5280852527741));
#71596=CARTESIAN_POINT('Ctrl Pts',(1.84657495109044,1.65617910540199,15.5246603905846));
#71597=CARTESIAN_POINT('Ctrl Pts',(1.90341295390484,1.59512114682347,15.5212504095826));
#71598=CARTESIAN_POINT('Ctrl Pts',(1.95689046613085,1.53122773141625,15.5178508639384));
#71599=CARTESIAN_POINT('Ctrl Pts',(2.01194103421405,1.46545487347031,15.5143513197161));
#71600=CARTESIAN_POINT('Ctrl Pts',(2.06343093897923,1.39667671283205,15.5108628337987));
#71601=CARTESIAN_POINT('Ctrl Pts',(2.11130423046702,1.3252770563036,15.507380556377));
#71602=CARTESIAN_POINT('Ctrl Pts',(2.15745742078722,1.25644281002257,15.5040233981871));
#71603=CARTESIAN_POINT('Ctrl Pts',(2.20024928268006,1.18517117106803,15.500672010362));
#71604=CARTESIAN_POINT('Ctrl Pts',(2.23959635988792,1.11177753196584,15.4973220472993));
#71605=CARTESIAN_POINT('Ctrl Pts',(2.25681070616636,1.07966781485864,15.4958564384594));
#71606=CARTESIAN_POINT('Ctrl Pts',(2.27336525378777,1.04715163497876,15.4943911023279));
#71607=CARTESIAN_POINT('Ctrl Pts',(2.28925084670373,1.0142542353915,15.4929256750031));
#71608=CARTESIAN_POINT('Ctrl Pts',(2.29885484868501,0.994365352899876,15.4920397170785));
#71609=CARTESIAN_POINT('Ctrl Pts',(2.30821431569525,0.974337119524171,15.491153725822));
#71610=CARTESIAN_POINT('Ctrl Pts',(2.3173269757796,0.954175024263046,15.4902676208197));
#71611=CARTESIAN_POINT('Ctrl Pts',(2.32227232757467,0.943233251710468,15.4897867402729));
#71612=CARTESIAN_POINT('Ctrl Pts',(2.32714420559321,0.932253683866113,15.4893058986854));
#71613=CARTESIAN_POINT('Ctrl Pts',(2.33193873109372,0.921245710398884,15.4888254510349));
#71614=CARTESIAN_POINT('Ctrl Pts',(2.36754247444614,0.839501424730483,15.4852576871677));
#71615=CARTESIAN_POINT('Ctrl Pts',(2.39894281260828,0.756064329075142,15.4817059560376));
#71616=CARTESIAN_POINT('Ctrl Pts',(2.42608268559146,0.671340103595013,15.4781652340513));
#71617=CARTESIAN_POINT('Ctrl Pts',(2.453534139292,0.58564319725637,15.4745838626229));
#71618=CARTESIAN_POINT('Ctrl Pts',(2.47662715562456,0.498628540954889,15.4710137545713));
#71619=CARTESIAN_POINT('Ctrl Pts',(2.49525785992387,0.410687466692489,15.4674497112883));
#71620=CARTESIAN_POINT('Ctrl Pts',(2.51258257274376,0.328910963121187,15.4641355034428));
#71621=CARTESIAN_POINT('Ctrl Pts',(2.52604844140045,0.24633247953868,15.4608265399003));
#71622=CARTESIAN_POINT('Ctrl Pts',(2.53553303361489,0.163255416668028,15.4575186404574));
#71623=CARTESIAN_POINT('Ctrl Pts',(2.53942998139287,0.129121426694033,15.4561595191486));
#71624=CARTESIAN_POINT('Ctrl Pts',(2.54265436806282,0.0949032017028567,
15.4548005774761));
#71625=CARTESIAN_POINT('Ctrl Pts',(2.54519570834653,0.0606216731012661,
15.4534415254952));
#71626=CARTESIAN_POINT('Ctrl Pts',(2.54650804671318,0.0429188233335401,
15.4527397162695));
#71627=CARTESIAN_POINT('Ctrl Pts',(2.5476382209856,0.0251990932110098,15.4520378776284));
#71628=CARTESIAN_POINT('Ctrl Pts',(2.54858465973821,0.00746537430393359,
15.4513359696452));
#71629=CARTESIAN_POINT('Ctrl Pts',(2.54936740774304,-0.00720121986763361,
15.4507554597369));
#71630=CARTESIAN_POINT('Ctrl Pts',(2.55002444266908,-0.0218786230829287,
15.4501748534934));
#71631=CARTESIAN_POINT('Ctrl Pts',(2.55055443165925,-0.0365475000712079,
15.4495948274855));
#71632=CARTESIAN_POINT('Ctrl Pts',(2.55387898415761,-0.128563471239416,
15.4459563992365));
#71633=CARTESIAN_POINT('Ctrl Pts',(2.55221836548087,-0.22040066645441,15.4423345418383));
#71634=CARTESIAN_POINT('Ctrl Pts',(2.5454697064449,-0.311650010793409,15.4387239299593));
#71635=CARTESIAN_POINT('Ctrl Pts',(2.53872104740894,-0.402899355132408,
15.4351133180804));
#71636=CARTESIAN_POINT('Ctrl Pts',(2.52688470709894,-0.49356189746232,15.4315139517205));
#71637=CARTESIAN_POINT('Ctrl Pts',(2.50980235603637,-0.583236219097685,
15.4279205055482));
#71638=CARTESIAN_POINT('Ctrl Pts',(2.49326213150481,-0.670064631014266,
15.424441101202));
#71639=CARTESIAN_POINT('Ctrl Pts',(2.47180332144007,-0.755967381987536,
15.420967247239));
#71640=CARTESIAN_POINT('Ctrl Pts',(2.44569482135312,-0.840684658565203,
15.4174941094224));
#71641=CARTESIAN_POINT('Ctrl Pts',(2.43658807165331,-0.870234384917672,
15.4162826650015));
#71642=CARTESIAN_POINT('Ctrl Pts',(2.42691516765274,-0.899639766052948,
15.41507130771));
#71643=CARTESIAN_POINT('Ctrl Pts',(2.41668612527745,-0.928889320342703,
15.4138598323975));
#71644=CARTESIAN_POINT('Ctrl Pts',(2.41079789512425,-0.945726488595391,
15.4131624606198));
#71645=CARTESIAN_POINT('Ctrl Pts',(2.40472537046329,-0.962512016907764,
15.4124650497348));
#71646=CARTESIAN_POINT('Ctrl Pts',(2.39847036187175,-0.979243667871416,
15.4117675606113));
#71647=CARTESIAN_POINT('Ctrl Pts',(2.39421301098727,-0.990631743201221,
15.4112928281));
#71648=CARTESIAN_POINT('Ctrl Pts',(2.38987156242605,-1.0019935463669,15.4108181134517));
#71649=CARTESIAN_POINT('Ctrl Pts',(2.38545028303317,-1.01331939423191,15.4103437824454));
#71650=CARTESIAN_POINT('Ctrl Pts',(2.35279097735238,-1.09698167717045,15.4068399728119));
#71651=CARTESIAN_POINT('Ctrl Pts',(2.31572987674733,-1.17881857921774,15.4033514296728));
#71652=CARTESIAN_POINT('Ctrl Pts',(2.27459874133947,-1.25857844945699,15.3998733992833));
#71653=CARTESIAN_POINT('Ctrl Pts',(2.23281288372258,-1.33960793109688,15.396340005877));
#71654=CARTESIAN_POINT('Ctrl Pts',(2.18682594253521,-1.41849449977561,15.3928174625663));
#71655=CARTESIAN_POINT('Ctrl Pts',(2.13693151879332,-1.49496175096055,15.3893007849646));
#71656=CARTESIAN_POINT('Ctrl Pts',(2.08679723793274,-1.57179660263405,15.385767201663));
#71657=CARTESIAN_POINT('Ctrl Pts',(2.03271725897117,-1.64618961960946,15.3822395406022));
#71658=CARTESIAN_POINT('Ctrl Pts',(1.97494281786374,-1.71783598585985,15.3787127451654));
#71659=CARTESIAN_POINT('Ctrl Pts',(1.95216878512211,-1.74607817495815,15.3773225222016));
#71660=CARTESIAN_POINT('Ctrl Pts',(1.92882022676702,-1.77389324483966,15.3759324337425));
#71661=CARTESIAN_POINT('Ctrl Pts',(1.90491084697345,-1.80126106485015,15.3745421700657));
#71662=CARTESIAN_POINT('Ctrl Pts',(1.89303589564547,-1.8148537022746,15.3738516748025));
#71663=CARTESIAN_POINT('Ctrl Pts',(1.88102258946071,-1.82833599951471,15.3731611363172));
#71664=CARTESIAN_POINT('Ctrl Pts',(1.86887253021617,-1.84170540057035,15.3724705166642));
#71665=CARTESIAN_POINT('Ctrl Pts',(1.86055716973053,-1.85085526453538,15.3719978645349));
#71666=CARTESIAN_POINT('Ctrl Pts',(1.8521789913077,-1.85995082597714,15.3715252464369));
#71667=CARTESIAN_POINT('Ctrl Pts',(1.84374494253208,-1.86898463564396,15.3710530027583));
#71668=CARTESIAN_POINT('Ctrl Pts',(1.77862481272331,-1.93873557897155,15.3674067623267));
#71669=CARTESIAN_POINT('Ctrl Pts',(1.71007452953627,-2.00492197279666,15.3637769310107));
#71670=CARTESIAN_POINT('Ctrl Pts',(1.63841756617314,-2.06724394639147,15.3601581531957));
#71671=CARTESIAN_POINT('Ctrl Pts',(1.56864469297252,-2.1279272764847,15.3566345245939));
#71672=CARTESIAN_POINT('Ctrl Pts',(1.49592552744324,-2.18494739655425,15.3531213758712));
#71673=CARTESIAN_POINT('Ctrl Pts',(1.42051657448793,-2.237996979208,15.3496137628515));
#71674=CARTESIAN_POINT('Ctrl Pts',(1.34626553575621,-2.29023197866037,15.3461600096832));
#71675=CARTESIAN_POINT('Ctrl Pts',(1.26940602418092,-2.33861808827242,15.3427116235202));
#71676=CARTESIAN_POINT('Ctrl Pts',(1.19015227451303,-2.38282228508801,15.3392638844625));
#71677=CARTESIAN_POINT('Ctrl Pts',(1.16438136391748,-2.39719614637352,15.3381427845096));
#71678=CARTESIAN_POINT('Ctrl Pts',(1.1383570943619,-2.4111274748391,15.3370217529787));
#71679=CARTESIAN_POINT('Ctrl Pts',(1.11208629310672,-2.42460372067378,15.3359006275904));
#71680=CARTESIAN_POINT('Ctrl Pts',(1.09252404263768,-2.4346386523776,15.3350657944447));
#71681=CARTESIAN_POINT('Ctrl Pts',(1.07282508844486,-2.44442123549769,15.3342309092564));
#71682=CARTESIAN_POINT('Ctrl Pts',(1.05299217133848,-2.4539460706498,15.3333959050218));
#71683=CARTESIAN_POINT('Ctrl Pts',(1.04038456497523,-2.46000092237074,15.3328651003678));
#71684=CARTESIAN_POINT('Ctrl Pts',(1.02772285622574,-2.46595150778408,15.3323342505181));
#71685=CARTESIAN_POINT('Ctrl Pts',(1.01502087310116,-2.47179063085649,15.3318038822616));
#71686=CARTESIAN_POINT('Ctrl Pts',(0.982652722257195,-2.48667032440912,
15.3304523578927));
#71687=CARTESIAN_POINT('Ctrl Pts',(0.950002091670773,-2.50083650005249,
15.3291030741213));
#71688=CARTESIAN_POINT('Ctrl Pts',(0.917084170499721,-2.5142729570447,15.3277557583224));
#71689=CARTESIAN_POINT('Ctrl Pts',(0.834495683370104,-2.5479839757206,15.3243754484619));
#71690=CARTESIAN_POINT('Ctrl Pts',(0.750226663082229,-2.57710500546031,
15.3210075263739));
#71691=CARTESIAN_POINT('Ctrl Pts',(0.664646844355562,-2.60177034865307,
15.317647686521));
#71692=CARTESIAN_POINT('Ctrl Pts',(0.576787650214132,-2.6270926408521,15.3141983590239));
#71693=CARTESIAN_POINT('Ctrl Pts',(0.487546169865586,-2.64771888106776,
15.3107575500279));
#71694=CARTESIAN_POINT('Ctrl Pts',(0.397298853288816,-2.66374516605354,
15.3073206007236));
#71695=CARTESIAN_POINT('Ctrl Pts',(0.308910977458226,-2.67944124812091,
15.3039544657529));
#71696=CARTESIAN_POINT('Ctrl Pts',(0.219557440695963,-2.69072476824651,
15.3005920330634));
#71697=CARTESIAN_POINT('Ctrl Pts',(0.129581594551193,-2.69764046998944,
15.2972289259214));
#71698=CARTESIAN_POINT('Ctrl Pts',(0.0974227261046785,-2.7001122571645,
15.2960268953233));
#71699=CARTESIAN_POINT('Ctrl Pts',(0.0651843226484069,-2.70202565483482,
15.2948247785662));
#71700=CARTESIAN_POINT('Ctrl Pts',(0.0328820436324132,-2.7033813247538,
15.2936223758136));
#71701=CARTESIAN_POINT('Ctrl Pts',(0.0192199250543532,-2.70395469987624,
15.2931138244208));
#71702=CARTESIAN_POINT('Ctrl Pts',(0.00555605037576419,-2.70442788901379,
15.2926055817652));
#71703=CARTESIAN_POINT('Ctrl Pts',(-0.00810768527292701,-2.70480131817288,
15.2920976575977));
#71704=CARTESIAN_POINT('Ctrl Pts',(-0.102177189495074,-2.70737223265483,
15.2886007973064));
#71705=CARTESIAN_POINT('Ctrl Pts',(-0.196248953232544,-2.705219350857,15.2851186519246));
#71706=CARTESIAN_POINT('Ctrl Pts',(-0.28992790026966,-2.69846111693802,
15.2816464960614));
#71707=CARTESIAN_POINT('Ctrl Pts',(-0.384721183626751,-2.69162249200534,
15.2781330379685));
#71708=CARTESIAN_POINT('Ctrl Pts',(-0.479113197863739,-2.68006831395088,
15.2746298084638));
#71709=CARTESIAN_POINT('Ctrl Pts',(-0.572703609774366,-2.66386867615587,
15.2711319115131));
#71710=CARTESIAN_POINT('Ctrl Pts',(-0.670406973022026,-2.64695712438838,
15.2674802949704));
#71711=CARTESIAN_POINT('Ctrl Pts',(-0.767237930320469,-2.62498318167097,
15.2638344899723));
#71712=CARTESIAN_POINT('Ctrl Pts',(-0.862734200133818,-2.5979664405403,
15.2601889262148));
#71713=CARTESIAN_POINT('Ctrl Pts',(-0.899309423475345,-2.58761898568426,
15.258792669493));
#71714=CARTESIAN_POINT('Ctrl Pts',(-0.935688693950487,-2.57653116703875,
15.2573964481588));
#71715=CARTESIAN_POINT('Ctrl Pts',(-0.971845190453781,-2.56470173355219,
15.2559999492582));
#71716=CARTESIAN_POINT('Ctrl Pts',(-0.985718422450195,-2.56016278506391,
15.2554641132369));
#71717=CARTESIAN_POINT('Ctrl Pts',(-0.999558849945709,-2.55551463851664,
15.2549282363508));
#71718=CARTESIAN_POINT('Ctrl Pts',(-1.01336493152648,-2.55075717270086,
15.254392300921));
#71719=CARTESIAN_POINT('Ctrl Pts',(-1.02713823497804,-2.5460110019675,15.2538576378986));
#71720=CARTESIAN_POINT('Ctrl Pts',(-1.0408680078023,-2.54115923920241,15.2533232792799));
#71721=CARTESIAN_POINT('Ctrl Pts',(-1.05455083068562,-2.53620294641156,
15.2527892870021));
#71722=CARTESIAN_POINT('Ctrl Pts',(-1.14480706402235,-2.50350966941525,
15.2492669048126));
#71723=CARTESIAN_POINT('Ctrl Pts',(-1.23304972084596,-2.46626241239109,
15.2457593395817));
#71724=CARTESIAN_POINT('Ctrl Pts',(-1.3188786706842,-2.42453542284507,15.242261762893));
#71725=CARTESIAN_POINT('Ctrl Pts',(-1.40341018907482,-2.38343919842613,
15.238817057246));
#71726=CARTESIAN_POINT('Ctrl Pts',(-1.48560133565556,-2.33799743942912,
15.2353820404405));
#71727=CARTESIAN_POINT('Ctrl Pts',(-1.56505752288372,-2.28823266258407,
15.2319520997326));
#71728=CARTESIAN_POINT('Ctrl Pts',(-1.59875150777533,-2.26712954025155,
15.2304976079627));
#71729=CARTESIAN_POINT('Ctrl Pts',(-1.63195344745741,-2.24524844976825,
15.2290440290004));
#71730=CARTESIAN_POINT('Ctrl Pts',(-1.66463195977674,-2.22258855435451,
15.2275910110965));
#71731=CARTESIAN_POINT('Ctrl Pts',(-1.74176819837999,-2.16910083489293,
15.2241612241271));
#71732=CARTESIAN_POINT('Ctrl Pts',(-1.81599039866318,-2.11127647963352,
15.2207345632396));
#71733=CARTESIAN_POINT('Ctrl Pts',(-1.88715256813859,-2.04946422501414,
15.2173064022613));
#71734=CARTESIAN_POINT('Ctrl Pts',(-1.90164577925548,-2.03687526008497,
15.2166082074035));
#71735=CARTESIAN_POINT('Ctrl Pts',(-1.91601194648249,-2.02412075255685,
15.215909950323));
#71736=CARTESIAN_POINT('Ctrl Pts',(-1.9302496520377,-2.01120346334021,15.2152115919387));
#71737=CARTESIAN_POINT('Ctrl Pts',(-1.94128816753001,-2.0011886687103,15.2146701535858));
#71738=CARTESIAN_POINT('Ctrl Pts',(-1.95224352654855,-1.99108137253609,
15.2141289446068));
#71739=CARTESIAN_POINT('Ctrl Pts',(-1.96311133771197,-1.98088698275119,
15.2135881466736));
#71740=CARTESIAN_POINT('Ctrl Pts',(-2.03178675603926,-1.91646702066845,
15.2101707589647));
#71741=CARTESIAN_POINT('Ctrl Pts',(-2.09701995613675,-1.8485265277173,15.2067672577273));
#71742=CARTESIAN_POINT('Ctrl Pts',(-2.15871310631003,-1.77747212767664,
15.2033732357386));
#71743=CARTESIAN_POINT('Ctrl Pts',(-2.22164945390415,-1.7049858888237,15.1999108197811));
#71744=CARTESIAN_POINT('Ctrl Pts',(-2.28090217022322,-1.62925832538052,
15.19645826896));
#71745=CARTESIAN_POINT('Ctrl Pts',(-2.33633512040192,-1.55067589533689,
15.1930109042136));
#71746=CARTESIAN_POINT('Ctrl Pts',(-2.39218601791983,-1.47150097801918,
15.1895375474008));
#71747=CARTESIAN_POINT('Ctrl Pts',(-2.44415984798534,-1.38942718616138,
15.1860694551604));
#71748=CARTESIAN_POINT('Ctrl Pts',(-2.49207710040016,-1.30481547317471,
15.1826018417945));
#71749=CARTESIAN_POINT('Ctrl Pts',(-2.52022211747796,-1.25511733759765,
15.1805650798249));
#71750=CARTESIAN_POINT('Ctrl Pts',(-2.54696681998739,-1.20454303320315,
15.1785284830672));
#71751=CARTESIAN_POINT('Ctrl Pts',(-2.57226731600719,-1.15316195438398,
15.1764910817393));
#71752=CARTESIAN_POINT('Ctrl Pts',(-2.57933924906923,-1.13880004030214,
15.1759215922795));
#71753=CARTESIAN_POINT('Ctrl Pts',(-2.58629893239321,-1.12437358425022,
15.1753519825172));
#71754=CARTESIAN_POINT('Ctrl Pts',(-2.59313735551554,-1.10990147500019,
15.1747829112963));
#71755=CARTESIAN_POINT('Ctrl Pts',(-2.63517066423893,-1.02094666405867,
15.1712850367298));
#71756=CARTESIAN_POINT('Ctrl Pts',(-2.6726976453638,-0.930127060905838,
15.167801819036));
#71757=CARTESIAN_POINT('Ctrl Pts',(-2.70558302354023,-0.837840896222647,
15.1643285389057));
#71758=CARTESIAN_POINT('Ctrl Pts',(-2.73847376195491,-0.745539689114618,
15.1608546926391));
#71759=CARTESIAN_POINT('Ctrl Pts',(-2.76672184052432,-0.651770570287676,
15.1573907871758));
#71760=CARTESIAN_POINT('Ctrl Pts',(-2.79014819101862,-0.556903769359717,
15.1539321008988));
#71761=CARTESIAN_POINT('Ctrl Pts',(-2.81305355218475,-0.464146754627161,
15.1505503339286));
#71762=CARTESIAN_POINT('Ctrl Pts',(-2.83134952927604,-0.370339481518358,
15.1471735565822));
#71763=CARTESIAN_POINT('Ctrl Pts',(-2.8448219024633,-0.275813943398833,
15.1437973553073));
#71764=CARTESIAN_POINT('Ctrl Pts',(-2.85447686455589,-0.208072315799913,
15.1413778042102));
#71765=CARTESIAN_POINT('Ctrl Pts',(-2.86165354894421,-0.139961477196466,
15.1389585489751));
#71766=CARTESIAN_POINT('Ctrl Pts',(-2.86625656775569,-0.071602632167948,
15.1365379651471));
#71767=CARTESIAN_POINT('Ctrl Pts',(-2.8678889837078,-0.0473598311579388,
15.1356795285827));
#71768=CARTESIAN_POINT('Ctrl Pts',(-2.86919553394546,-0.0231160969724086,
15.1348219958471));
#71769=CARTESIAN_POINT('Ctrl Pts',(-2.87017396612668,0.00112290304428943,
15.1339652973708));
#71770=CARTESIAN_POINT('',(0.261080338132197,2.92584241055005,15.058));
#71771=CARTESIAN_POINT('Ctrl Pts',(0.260984867623723,2.92515103163649,15.058));
#71772=CARTESIAN_POINT('Ctrl Pts',(0.163110290089364,2.92129299518303,15.0703787026841));
#71773=CARTESIAN_POINT('Ctrl Pts',(0.0656985383021158,2.91278590387498,
15.0828015605825));
#71774=CARTESIAN_POINT('Ctrl Pts',(-0.0308724856851826,2.89964343902045,
15.0952881213498));
#71775=CARTESIAN_POINT('Ctrl Pts',(-0.13093434020212,2.88602590291106,15.1082260438789));
#71776=CARTESIAN_POINT('Ctrl Pts',(-0.230094798512676,2.86743186329655,
15.121232357953));
#71777=CARTESIAN_POINT('Ctrl Pts',(-0.327908726704405,2.84382209488468,
15.1343288085909));
#71778=CARTESIAN_POINT('Ctrl Pts',(-0.401269172848201,2.82611476857578,
15.1441511465694));
#71779=CARTESIAN_POINT('Ctrl Pts',(-0.473871776581697,2.80558493098147,
15.154024186365));
#71780=CARTESIAN_POINT('Ctrl Pts',(-0.54551386023679,2.78219703023119,15.1639571016578));
#71781=CARTESIAN_POINT('Ctrl Pts',(-0.599245422978111,2.76465610466849,
15.1714067881273));
#71782=CARTESIAN_POINT('Ctrl Pts',(-0.652436445713434,2.74550717996222,
15.178890154564));
#71783=CARTESIAN_POINT('Ctrl Pts',(-0.704995275147146,2.7247296345796,15.186411071114));
#71784=CARTESIAN_POINT('Ctrl Pts',(-0.720729468886594,2.71850959642421,
15.1886625588158));
#71785=CARTESIAN_POINT('Ctrl Pts',(-0.736406966678059,2.71214357207348,
15.1909174117022));
#71786=CARTESIAN_POINT('Ctrl Pts',(-0.752025204049111,2.70563092815761,
15.1931757336031));
#71787=CARTESIAN_POINT('Ctrl Pts',(-0.764775912501757,2.70031401422844,
15.1950194246335));
#71788=CARTESIAN_POINT('Ctrl Pts',(-0.777478081511626,2.69490314594757,
15.196864120682));
#71789=CARTESIAN_POINT('Ctrl Pts',(-0.790130440968904,2.6893983882733,15.1987098648068));
#71790=CARTESIAN_POINT('Ctrl Pts',(-0.873485337988913,2.65313254310755,
15.2108697952897));
#71791=CARTESIAN_POINT('Ctrl Pts',(-0.954683148186728,2.61279395749136,
15.2230755503321));
#71792=CARTESIAN_POINT('Ctrl Pts',(-1.0333900295422,2.56835839969231,15.2353460721376));
#71793=CARTESIAN_POINT('Ctrl Pts',(-1.07474974365993,2.54500793864519,15.2417941141031));
#71794=CARTESIAN_POINT('Ctrl Pts',(-1.11542111238663,2.52052546068703,15.2482600407761));
#71795=CARTESIAN_POINT('Ctrl Pts',(-1.15535178122673,2.49490314259947,15.2547466008415));
#71796=CARTESIAN_POINT('Ctrl Pts',(-1.23327915249916,2.44489947493076,15.2674055567063));
#71797=CARTESIAN_POINT('Ctrl Pts',(-1.30838829429154,2.39055588937394,15.2801430971848));
#71798=CARTESIAN_POINT('Ctrl Pts',(-1.38046450469962,2.33219918561456,15.2929796526032));
#71799=CARTESIAN_POINT('Ctrl Pts',(-1.45426350057602,2.27244762382022,15.3061230309111));
#71800=CARTESIAN_POINT('Ctrl Pts',(-1.52488347180723,2.20848778279982,15.3193702140928));
#71801=CARTESIAN_POINT('Ctrl Pts',(-1.59204074405781,2.14065188994946,15.332743132764));
#71802=CARTESIAN_POINT('Ctrl Pts',(-1.60237109058904,2.13021715582588,15.3348001979094));
#71803=CARTESIAN_POINT('Ctrl Pts',(-1.61262065491134,2.1196893711682,15.3368604944486));
#71804=CARTESIAN_POINT('Ctrl Pts',(-1.62278430900332,2.10907388768773,15.3389232952054));
#71805=CARTESIAN_POINT('Ctrl Pts',(-1.68486768809848,2.04423056665054,15.3515236493914));
#71806=CARTESIAN_POINT('Ctrl Pts',(-1.74353795945352,1.97633977637267,15.3641743680265));
#71807=CARTESIAN_POINT('Ctrl Pts',(-1.79863355499942,1.90572574364455,15.3768970731667));
#71808=CARTESIAN_POINT('Ctrl Pts',(-1.8536060338742,1.83526950510231,15.3895913481376));
#71809=CARTESIAN_POINT('Ctrl Pts',(-1.90502010402237,1.76210117952091,15.4023572882508));
#71810=CARTESIAN_POINT('Ctrl Pts',(-1.95266740197694,1.68652354076833,15.4152163709358));
#71811=CARTESIAN_POINT('Ctrl Pts',(-1.999553014057,1.61215408007279,15.4278698893587));
#71812=CARTESIAN_POINT('Ctrl Pts',(-2.04279147033365,1.53545080587127,15.4406135962167));
#71813=CARTESIAN_POINT('Ctrl Pts',(-2.08213462636226,1.45669772176484,15.4534679553077));
#71814=CARTESIAN_POINT('Ctrl Pts',(-2.10370638024081,1.41351760306046,15.4605159681915));
#71815=CARTESIAN_POINT('Ctrl Pts',(-2.12410620181193,1.36972125073741,15.4675972464718));
#71816=CARTESIAN_POINT('Ctrl Pts',(-2.14328646703913,1.32535636167276,15.4747151632939));
#71817=CARTESIAN_POINT('Ctrl Pts',(-2.15012579550102,1.30953666132481,15.4772532810172));
#71818=CARTESIAN_POINT('Ctrl Pts',(-2.15681001155505,1.29364468163272,15.4797960573454));
#71819=CARTESIAN_POINT('Ctrl Pts',(-2.16333680365848,1.27768262506038,15.4823436452153));
#71820=CARTESIAN_POINT('Ctrl Pts',(-2.16791412260327,1.2664882400105,15.4841302996752));
#71821=CARTESIAN_POINT('Ctrl Pts',(-2.17241292255598,1.25526195256421,15.4859189101699));
#71822=CARTESIAN_POINT('Ctrl Pts',(-2.17682958710993,1.24401228867859,15.4877083034276));
#71823=CARTESIAN_POINT('Ctrl Pts',(-2.20791015801245,1.16484712416239,15.5003004673422));
#71824=CARTESIAN_POINT('Ctrl Pts',(-2.2349734122897,1.08441291813616,15.5129492481641));
#71825=CARTESIAN_POINT('Ctrl Pts',(-2.25783961089921,1.00297802743715,15.5256767231474));
#71826=CARTESIAN_POINT('Ctrl Pts',(-2.28035828534265,0.922780797311416,
15.5382107639178));
#71827=CARTESIAN_POINT('Ctrl Pts',(-2.29880657051476,0.841612257746407,
15.5508211250137));
#71828=CARTESIAN_POINT('Ctrl Pts',(-2.31296316132111,0.759731453145844,
15.5635288923091));
#71829=CARTESIAN_POINT('Ctrl Pts',(-2.32670958827523,0.680223009708963,
15.5758684730222));
#71830=CARTESIAN_POINT('Ctrl Pts',(-2.33640931253598,0.600042348520933,
15.5882998973352));
#71831=CARTESIAN_POINT('Ctrl Pts',(-2.34181299591968,0.519439649300842,
15.6008424709262));
#71832=CARTESIAN_POINT('Ctrl Pts',(-2.34572284670801,0.461119332452094,
15.609917686434));
#71833=CARTESIAN_POINT('Ctrl Pts',(-2.34738263953658,0.402578305857885,
15.6190510917899));
#71834=CARTESIAN_POINT('Ctrl Pts',(-2.34668236863854,0.343918483395394,
15.62825));
#71835=CARTESIAN_POINT('',(-2.14373220034752,2.0119373894844,15.058));
#71836=CARTESIAN_POINT('Origin',(0.,0.,15.058));
#71837=CARTESIAN_POINT('Ctrl Pts',(-2.87017396612668,0.00112290304428943,
15.1339652973708));
#71838=CARTESIAN_POINT('Ctrl Pts',(-2.87266912500978,0.0629362380616879,
15.1317805789463));
#71839=CARTESIAN_POINT('Ctrl Pts',(-2.87303098230106,0.124718621761705,
15.1296012856735));
#71840=CARTESIAN_POINT('Ctrl Pts',(-2.87121685856479,0.18637804904607,15.1274262638706));
#71841=CARTESIAN_POINT('Ctrl Pts',(-2.86841400163638,0.281643079490827,
15.1240658123162));
#71842=CARTESIAN_POINT('Ctrl Pts',(-2.86041988710444,0.376614623554742,
15.1207155571276));
#71843=CARTESIAN_POINT('Ctrl Pts',(-2.84750858059062,0.47099184224787,15.1173712434175));
#71844=CARTESIAN_POINT('Ctrl Pts',(-2.83433033308302,0.567320307975548,
15.1139577860911));
#71845=CARTESIAN_POINT('Ctrl Pts',(-2.81602924148459,0.663030385704492,
15.1105505184628));
#71846=CARTESIAN_POINT('Ctrl Pts',(-2.79284156103339,0.757800921120369,
15.1071449162423));
#71847=CARTESIAN_POINT('Ctrl Pts',(-2.77879319434313,0.815218101582043,
15.1050816159094));
#71848=CARTESIAN_POINT('Ctrl Pts',(-2.76295010551778,0.872290339259573,
15.1030189268812));
#71849=CARTESIAN_POINT('Ctrl Pts',(-2.74535586092349,0.928944130664371,
15.100955843023));
#71850=CARTESIAN_POINT('Ctrl Pts',(-2.7354097693855,0.960970728468381,15.099789574088));
#71851=CARTESIAN_POINT('Ctrl Pts',(-2.72490394590206,0.992863566804536,
15.098623178978));
#71852=CARTESIAN_POINT('Ctrl Pts',(-2.7138453785436,1.0246089965303,15.0974564759315));
#71853=CARTESIAN_POINT('Ctrl Pts',(-2.70868377697821,1.03942621963478,15.0969119156755));
#71854=CARTESIAN_POINT('Ctrl Pts',(-2.7034040983514,1.05420445638712,15.0963675402945));
#71855=CARTESIAN_POINT('Ctrl Pts',(-2.69801003661965,1.06893536837389,15.0958235919881));
#71856=CARTESIAN_POINT('Ctrl Pts',(-2.66394262772994,1.16197175299988,15.0923881642358));
#71857=CARTESIAN_POINT('Ctrl Pts',(-2.62528653689294,1.25320878716493,15.0889665364856));
#71858=CARTESIAN_POINT('Ctrl Pts',(-2.58232115247044,1.34232723597939,15.0855542358814));
#71859=CARTESIAN_POINT('Ctrl Pts',(-2.53887733631532,1.43243804397901,15.0821039383428));
#71860=CARTESIAN_POINT('Ctrl Pts',(-2.49102735184572,1.52038366982231,15.0786631768276));
#71861=CARTESIAN_POINT('Ctrl Pts',(-2.43900735397324,1.60582293428401,15.0752273273902));
#71862=CARTESIAN_POINT('Ctrl Pts',(-2.38725398360023,1.69082428143753,15.071809088333));
#71863=CARTESIAN_POINT('Ctrl Pts',(-2.33137274895099,1.77334571203064,15.0683957111292));
#71864=CARTESIAN_POINT('Ctrl Pts',(-2.27155099682431,1.8530278346518,15.064982642569));
#71865=CARTESIAN_POINT('Ctrl Pts',(-2.23076137590659,1.90735930205439,15.0626554326866));
#71866=CARTESIAN_POINT('Ctrl Pts',(-2.18813878650124,1.96037022431859,15.0603283662998));
#71867=CARTESIAN_POINT('Ctrl Pts',(-2.14373220034752,2.0119373894844,15.058));
#71868=CARTESIAN_POINT('',(-2.,-2.44929359829471E-16,16.));
#71869=CARTESIAN_POINT('',(-2.5,-3.06161699786838E-16,15.5));
#71870=CARTESIAN_POINT('Origin',(0.,0.,16.));
#71871=CARTESIAN_POINT('Ctrl Pts',(1.70810875200393,-2.39535560853239,-0.329233991005387));
#71872=CARTESIAN_POINT('Ctrl Pts',(2.5000696979919,-1.83061464970825,-0.276613620635017));
#71873=CARTESIAN_POINT('Ctrl Pts',(3.46698259537958,0.135843711197753,-0.171372879894276));
#71874=CARTESIAN_POINT('Ctrl Pts',(1.78000461065578,2.98198357260362,-0.013511768783165));
#71875=CARTESIAN_POINT('Ctrl Pts',(-1.52068059202578,3.11864337292237,0.144349342327946));
#71876=CARTESIAN_POINT('Ctrl Pts',(-3.44323740053193,0.434868872546417,
0.302210453439058));
#71877=CARTESIAN_POINT('Ctrl Pts',(-2.24748662857037,-2.64500439253867,
0.460071564550167));
#71878=CARTESIAN_POINT('Ctrl Pts',(0.98413688813967,-3.32800743087112,0.61793267566128));
#71879=CARTESIAN_POINT('Ctrl Pts',(3.3242675736315,-0.997273536182889,0.775793786772391));
#71880=CARTESIAN_POINT('Ctrl Pts',(2.65350107828341,2.23705783115145,0.933654897883501));
#71881=CARTESIAN_POINT('Ctrl Pts',(-0.420704297245377,3.44500822120461,
1.09151600899461));
#71882=CARTESIAN_POINT('Ctrl Pts',(-3.11384086799285,1.53272940938773,1.24937712010572));
#71883=CARTESIAN_POINT('Ctrl Pts',(-2.98662452021757,-1.76786447124123,
1.40723823121684));
#71884=CARTESIAN_POINT('Ctrl Pts',(-0.154268773033873,-3.46719137695888,
1.56509934232795));
#71885=CARTESIAN_POINT('Ctrl Pts',(2.81781362814421,-2.02612228753563,1.72296045343906));
#71886=CARTESIAN_POINT('Ctrl Pts',(3.23766264061691,1.25011350527631,1.88082156455017));
#71887=CARTESIAN_POINT('Ctrl Pts',(0.724998218776244,3.39405562633926,2.03868267566128));
#71888=CARTESIAN_POINT('Ctrl Pts',(-2.44433298400306,2.46383378430329,2.19654378677239));
#71889=CARTESIAN_POINT('Ctrl Pts',(-3.39970985401105,-0.698006346200326,
2.35440489788351));
#71890=CARTESIAN_POINT('Ctrl Pts',(-1.27579956793912,-3.22762676650925,
2.51226600899461));
#71891=CARTESIAN_POINT('Ctrl Pts',(2.00366607964198,-2.83382462640088,2.67012712010573));
#71892=CARTESIAN_POINT('Ctrl Pts',(3.46831127903076,0.12671419166248,2.82798823121683));
#71893=CARTESIAN_POINT('Ctrl Pts',(1.79153366111842,2.9724815653929,2.98584934232795));
#71894=CARTESIAN_POINT('Ctrl Pts',(-1.50792549309295,3.12592391504671,3.14371045343906));
#71895=CARTESIAN_POINT('Ctrl Pts',(-3.44158119482194,0.448060782465637,
3.30157156455017));
#71896=CARTESIAN_POINT('Ctrl Pts',(-2.25802486298351,-2.63563337612261,
3.45943267566128));
#71897=CARTESIAN_POINT('Ctrl Pts',(0.970737398643871,-3.33210271331857,
3.61729378677239));
#71898=CARTESIAN_POINT('Ctrl Pts',(3.32025430017048,-1.01052014634333,3.7751548978835));
#71899=CARTESIAN_POINT('Ctrl Pts',(2.66245099976358,2.22634100195603,3.93301600899462));
#71900=CARTESIAN_POINT('Ctrl Pts',(-0.406867188726441,3.44669387613558,
4.09087712010572));
#71901=CARTESIAN_POINT('Ctrl Pts',(-3.10766543711734,1.54520390729755,4.24873823121684));
#71902=CARTESIAN_POINT('Ctrl Pts',(-2.99369583814259,-1.75585443953709,
4.40659934232795));
#71903=CARTESIAN_POINT('Ctrl Pts',(-0.16818635164463,-3.46654769699322,
4.56446045343906));
#71904=CARTESIAN_POINT('Ctrl Pts',(2.80965791624474,-2.03741551431062,4.72232156455017));
#71905=CARTESIAN_POINT('Ctrl Pts',(3.24265463709948,1.23710569022097,4.88018267566128));
#71906=CARTESIAN_POINT('Ctrl Pts',(0.738617048059715,3.39111846455234,5.0380437867724));
#71907=CARTESIAN_POINT('Ctrl Pts',(-2.43442290318405,2.47362582310745,5.1959048978835));
#71908=CARTESIAN_POINT('Ctrl Pts',(-3.40248440570545,-0.684353310232048,
5.35376600899462));
#71909=CARTESIAN_POINT('Ctrl Pts',(-1.28874579170717,-3.22247945977245,
5.51162712010572));
#71910=CARTESIAN_POINT('Ctrl Pts',(1.99227427239527,-2.84184496548404,5.66948823121683));
#71911=CARTESIAN_POINT('Ctrl Pts',(3.46879199270663,0.112790494414327,5.82734934232795));
#71912=CARTESIAN_POINT('Ctrl Pts',(1.803451502182,2.96526596843754,5.98521045343906));
#71913=CARTESIAN_POINT('Ctrl Pts',(-1.49536511544646,3.13195190828366,6.14307156455017));
#71914=CARTESIAN_POINT('Ctrl Pts',(-3.4397548386282,0.461872530499354,6.30093267566129));
#71915=CARTESIAN_POINT('Ctrl Pts',(-2.26858675213732,-2.62654787360198,
6.45879378677239));
#71916=CARTESIAN_POINT('Ctrl Pts',(0.957353695793138,-3.33597264458916,
6.61665489788351));
#71917=CARTESIAN_POINT('Ctrl Pts',(3.31617107144768,-1.02384032406894,6.77451600899461));
#71918=CARTESIAN_POINT('Ctrl Pts',(2.67136662968815,2.21563532967061,6.93237712010573));
#71919=CARTESIAN_POINT('Ctrl Pts',(-0.393028031746144,3.44829937078522,
7.09023823121684));
#71920=CARTESIAN_POINT('Ctrl Pts',(-3.10143756889894,1.55766639256237,7.24809934232795));
#71921=CARTESIAN_POINT('Ctrl Pts',(-3.00072015011765,-1.74382285940228,
7.40596045343905));
#71922=CARTESIAN_POINT('Ctrl Pts',(-0.182100573498421,-3.46584462511342,
7.56382156455018));
#71923=CARTESIAN_POINT('Ctrl Pts',(2.80145659039814,-2.04867775807003,7.72168267566128));
#71924=CARTESIAN_POINT('Ctrl Pts',(3.24759455782818,1.22407890769377,7.8795437867724));
#71925=CARTESIAN_POINT('Ctrl Pts',(0.752223882355328,3.38812615100299,8.03740489788349));
#71926=CARTESIAN_POINT('Ctrl Pts',(-2.42447354494764,2.4833782664236,8.19526600899462));
#71927=CARTESIAN_POINT('Ctrl Pts',(-3.40520415435994,-0.670689385204343,
8.35312712010572));
#71928=CARTESIAN_POINT('Ctrl Pts',(-1.30167123501543,-3.21728015258687,
8.51098823121684));
#71929=CARTESIAN_POINT('Ctrl Pts',(1.98085035420065,-2.84981954842042,8.66884934232795));
#71930=CARTESIAN_POINT('Ctrl Pts',(3.46921681308078,0.098864999537257,8.82671045343906));
#71931=CARTESIAN_POINT('Ctrl Pts',(1.81534028008778,2.95800257805621,8.98457156455017));
#71932=CARTESIAN_POINT('Ctrl Pts',(-1.4827806401293,3.13792943795007,9.14243267566127));
#71933=CARTESIAN_POINT('Ctrl Pts',(-3.4378730539225,0.475676832953572,9.3002937867724));
#71934=CARTESIAN_POINT('Ctrl Pts',(-2.27911208446667,-2.61742004476474,
9.45815489788349));
#71935=CARTESIAN_POINT('Ctrl Pts',(0.943954565772613,-3.3397888199782,9.61601600899462));
#71936=CARTESIAN_POINT('Ctrl Pts',(3.31203440522278,-1.03714400297725,9.77387712010572));
#71937=CARTESIAN_POINT('Ctrl Pts',(2.68023921253269,2.20489395389312,9.93173823121684));
#71938=CARTESIAN_POINT('Ctrl Pts',(-0.379182541400898,3.44984929882113,
10.0895993423279));
#71939=CARTESIAN_POINT('Ctrl Pts',(-3.09515972337558,1.57010377716378,10.2474604534391));
#71940=CARTESIAN_POINT('Ctrl Pts',(-3.00769610777576,-1.73176317886687,
10.4053215645502));
#71941=CARTESIAN_POINT('Ctrl Pts',(-0.196011860918037,-3.46508570377902,
10.5631826756613));
#71942=CARTESIAN_POINT('Ctrl Pts',(2.79321012116224,-2.05990698897259,10.7210437867724));
#71943=CARTESIAN_POINT('Ctrl Pts',(3.25248214612884,1.2110324001305,10.8789048978835));
#71944=CARTESIAN_POINT('Ctrl Pts',(0.765818594962506,3.38507924024569,11.0367660089946));
#71945=CARTESIAN_POINT('Ctrl Pts',(-2.41448511783304,2.49309069223908,11.1946271201057));
#71946=CARTESIAN_POINT('Ctrl Pts',(-3.40786903136843,-0.657014653010787,
11.3524882312168));
#71947=CARTESIAN_POINT('Ctrl Pts',(-1.3145757016765,-3.21202900045202,11.510349342328));
#71948=CARTESIAN_POINT('Ctrl Pts',(1.96939451380669,-2.85774821044889,11.668210453439));
#71949=CARTESIAN_POINT('Ctrl Pts',(3.46958573405997,0.0849379149034097,
11.8260715645502));
#71950=CARTESIAN_POINT('Ctrl Pts',(1.82719979676502,2.95069151525923,11.9839326756613));
#71951=CARTESIAN_POINT('Ctrl Pts',(-1.47017225488226,3.14385641459579,12.1417937867724));
#71952=CARTESIAN_POINT('Ctrl Pts',(-3.43593590116163,0.489473446687968,
12.2996548978835));
#71953=CARTESIAN_POINT('Ctrl Pts',(-2.28960063207268,-2.60824999320481,
12.4575160089946));
#71954=CARTESIAN_POINT('Ctrl Pts',(0.930540112760845,-3.34355126315401,
12.6153771201057));
#71955=CARTESIAN_POINT('Ctrl Pts',(3.30784458181684,-1.05043080491032,12.7732382312169));
#71956=CARTESIAN_POINT('Ctrl Pts',(2.68906819704165,2.19411673426304,12.9310993423279));
#71957=CARTESIAN_POINT('Ctrl Pts',(-0.365330160772045,3.45134423437463,
13.0889604534391));
#71958=CARTESIAN_POINT('Ctrl Pts',(-3.08883349189378,1.58251471600082,13.2468215645502));
#71959=CARTESIAN_POINT('Ctrl Pts',(-3.01462075186278,-1.71967340539697,
13.4046826756613));
#71960=CARTESIAN_POINT('Ctrl Pts',(-0.209925428309919,-3.46427512302224,
13.5625437867724));
#71961=CARTESIAN_POINT('Ctrl Pts',(2.78492903121011,-2.07109504482717,13.7204048978835));
#71962=CARTESIAN_POINT('Ctrl Pts',(3.25729747472216,1.19795113049603,13.8782660089946));
#71963=CARTESIAN_POINT('Ctrl Pts',(0.779438885227093,3.38200690959721,14.0361271201057));
#71964=CARTESIAN_POINT('Ctrl Pts',(-2.40453022224261,2.50270729758603,14.1939882312168));
#71965=CARTESIAN_POINT('Ctrl Pts',(-3.41034060095634,-0.643223025084935,
14.351849342328));
#71966=CARTESIAN_POINT('Ctrl Pts',(-1.3277234162215,-3.20692920286191,14.5097104534391));
#71967=CARTESIAN_POINT('Ctrl Pts',(1.95841253548915,-2.86524258546647,14.6675715645502));
#71968=CARTESIAN_POINT('Ctrl Pts',(3.46892903525912,0.0702659147297645,
14.8254326756613));
#71969=CARTESIAN_POINT('Ctrl Pts',(1.8409162673649,2.94476989555806,14.9832937867724));
#71970=CARTESIAN_POINT('Ctrl Pts',(-1.46144261101867,3.14684084841223,15.1411548978835));
#71971=CARTESIAN_POINT('Ctrl Pts',(-2.76985851330384,1.3890220685151,15.2463956386242));
#71972=CARTESIAN_POINT('Ctrl Pts',(-2.91090525077878,0.426608275808748,
15.2990160089946));
#71973=CARTESIAN_POINT('Ctrl Pts',(1.59774743137963,-2.24059110187414,-0.219489327336926));
#71974=CARTESIAN_POINT('Ctrl Pts',(2.33853958862414,-1.71233819332979,-0.166868956966556));
#71975=CARTESIAN_POINT('Ctrl Pts',(3.24298000926863,0.127066816079881,-0.061628216225815));
#71976=CARTESIAN_POINT('Ctrl Pts',(1.66499808117169,2.78931689094975,0.0962328948852963));
#71977=CARTESIAN_POINT('Ctrl Pts',(-1.42242905026252,2.9171470684346,0.254094005996407));
#71978=CARTESIAN_POINT('Ctrl Pts',(-3.22076899721748,0.406771889250497,
0.411955117107519));
#71979=CARTESIAN_POINT('Ctrl Pts',(-2.10227597256058,-2.4741100174146,0.56981622821863));
#71980=CARTESIAN_POINT('Ctrl Pts',(0.9205515651778,-3.11298406383574,0.72767733932974));
#71981=CARTESIAN_POINT('Ctrl Pts',(3.10948583967916,-0.932839451205724,
0.885538450440853));
#71982=CARTESIAN_POINT('Ctrl Pts',(2.48205773023319,2.09252098227156,1.04339956155196));
#71983=CARTESIAN_POINT('Ctrl Pts',(-0.393522490594119,3.22242540473713,
1.20126067266308));
#71984=CARTESIAN_POINT('Ctrl Pts',(-2.91265485451303,1.43369939061326,1.35912178377418));
#71985=CARTESIAN_POINT('Ctrl Pts',(-2.79365798581306,-1.65364231910831,
1.5169828948853));
#71986=CARTESIAN_POINT('Ctrl Pts',(-0.144301430203291,-3.24317530141947,
1.67484400599641));
#71987=CARTESIAN_POINT('Ctrl Pts',(2.6357540064074,-1.8952140352733,1.83270511710752));
#71988=CARTESIAN_POINT('Ctrl Pts',(3.02847647238534,1.16934336859111,1.99056622821863));
#71989=CARTESIAN_POINT('Ctrl Pts',(0.67815590807408,3.17476486938028,2.14842733932974));
#71990=CARTESIAN_POINT('Ctrl Pts',(-2.28640403724036,2.30464488610489,2.30628845044085));
#71991=CARTESIAN_POINT('Ctrl Pts',(-3.18005377603123,-0.652907986929923,
2.46414956155196));
#71992=CARTESIAN_POINT('Ctrl Pts',(-1.19336984851725,-3.01908901853714,
2.62201067266307));
#71993=CARTESIAN_POINT('Ctrl Pts',(1.87420872841654,-2.65073053018457,2.77987178377419));
#71994=CARTESIAN_POINT('Ctrl Pts',(3.24422284634695,0.118527157015377,2.9377328948853));
#71995=CARTESIAN_POINT('Ctrl Pts',(1.67578223688854,2.78042881072881,3.09559400599641));
#71996=CARTESIAN_POINT('Ctrl Pts',(-1.41049806136441,2.92395721296701,3.25345511710752));
#71997=CARTESIAN_POINT('Ctrl Pts',(-3.21921979935999,0.419111466671254,
3.41131622821863));
#71998=CARTESIAN_POINT('Ctrl Pts',(-2.11213332909314,-2.46534446464132,
3.56917733932974));
#71999=CARTESIAN_POINT('Ctrl Pts',(0.908017819947236,-3.11681474909129,
3.72703845044085));
#72000=CARTESIAN_POINT('Ctrl Pts',(3.10573186478955,-0.94523019467185,3.88489956155197));
#72001=CARTESIAN_POINT('Ctrl Pts',(2.49042939511648,2.08249657000891,4.04276067266307));
#72002=CARTESIAN_POINT('Ctrl Pts',(-0.380579401011611,3.2240021490943,4.20062178377419));
#72003=CARTESIAN_POINT('Ctrl Pts',(-2.90687841972373,1.44536790818848,4.3584828948853));
#72004=CARTESIAN_POINT('Ctrl Pts',(-2.8002724241724,-1.64240825846459,4.5163440059964));
#72005=CARTESIAN_POINT('Ctrl Pts',(-0.157319790685473,-3.24257320977247,
4.67420511710753));
#72006=CARTESIAN_POINT('Ctrl Pts',(2.62812523703122,-1.90577760392813,4.83206622821863));
#72007=CARTESIAN_POINT('Ctrl Pts',(3.03314593476479,1.15717599162043,4.98992733932975));
#72008=CARTESIAN_POINT('Ctrl Pts',(0.690894821495446,3.17201747832858,5.14778845044085));
#72009=CARTESIAN_POINT('Ctrl Pts',(-2.27713424914591,2.31380425890769,5.30564956155197));
#72010=CARTESIAN_POINT('Ctrl Pts',(-3.18264906326793,-0.640137076925948,
5.46351067266308));
#72011=CARTESIAN_POINT('Ctrl Pts',(-1.20547961362863,-3.01427428053665,
5.62137178377419));
#72012=CARTESIAN_POINT('Ctrl Pts',(1.86355294859817,-2.65823267321491,5.7792328948853));
#72013=CARTESIAN_POINT('Ctrl Pts',(3.24467250099567,0.105503073222438,5.93709400599641));
#72014=CARTESIAN_POINT('Ctrl Pts',(1.68693006335134,2.77367941524228,6.09495511710752));
#72015=CARTESIAN_POINT('Ctrl Pts',(-1.39874921276312,2.92959573609933,6.25281622821863));
#72016=CARTESIAN_POINT('Ctrl Pts',(-3.21751144448276,0.432030834315646,
6.41067733932974));
#72017=CARTESIAN_POINT('Ctrl Pts',(-2.12201281202782,-2.45684597864148,
6.56853845044085));
#72018=CARTESIAN_POINT('Ctrl Pts',(0.895498841382776,-3.12043464316416,
6.72639956155197));
#72019=CARTESIAN_POINT('Ctrl Pts',(3.10191245446456,-0.957689752484927,
6.88426067266308));
#72020=CARTESIAN_POINT('Ctrl Pts',(2.4987689840299,2.07248259380561,7.04212178377418));
#72021=CARTESIAN_POINT('Ctrl Pts',(-0.367634395319329,3.22550391234535,
7.1999828948853));
#72022=CARTESIAN_POINT('Ctrl Pts',(-2.90105293558095,1.45702518925863,7.3578440059964));
#72023=CARTESIAN_POINT('Ctrl Pts',(-2.8068428936476,-1.63115404163953,7.51570511710752));
#72024=CARTESIAN_POINT('Ctrl Pts',(-0.170335011291572,-3.24191556353729,
7.67356622821863));
#72025=CARTESIAN_POINT('Ctrl Pts',(2.62045380083611,-1.91631219138755,7.83142733932975));
#72026=CARTESIAN_POINT('Ctrl Pts',(3.03776668601744,1.14499087267086,7.98928845044085));
#72027=CARTESIAN_POINT('Ctrl Pts',(0.703622514928034,3.16921849888318,8.14714956155197));
#72028=CARTESIAN_POINT('Ctrl Pts',(-2.26782772135753,2.32292659449655,8.30501067266308));
#72029=CARTESIAN_POINT('Ctrl Pts',(-3.18519308830241,-0.627355981407313,
8.46287178377418));
#72030=CARTESIAN_POINT('Ctrl Pts',(-1.21756994091078,-3.00941090184898,
8.62073289488531));
#72031=CARTESIAN_POINT('Ctrl Pts',(1.852867132528,-2.6656920164142,8.77859400599641));
#72032=CARTESIAN_POINT('Ctrl Pts',(3.24506987362244,0.0924773079458306,
8.93645511710752));
#72033=CARTESIAN_POINT('Ctrl Pts',(1.698050704434,2.7668853142746,9.09431622821864));
#72034=CARTESIAN_POINT('Ctrl Pts',(-1.3869778234475,2.93518705612466,9.25217733932973));
#72035=CARTESIAN_POINT('Ctrl Pts',(-3.21575124234316,0.444943237441223,
9.41003845044086));
#72036=CARTESIAN_POINT('Ctrl Pts',(-2.13185810008334,-2.44830790103859,
9.56789956155196));
#72037=CARTESIAN_POINT('Ctrl Pts',(0.882965432401702,-3.12400425453603,
9.72576067266308));
#72038=CARTESIAN_POINT('Ctrl Pts',(3.09804305924746,-0.970133877473286,
9.88362178377418));
#72039=CARTESIAN_POINT('Ctrl Pts',(2.50706830714555,2.06243522092151,10.0414828948853));
#72040=CARTESIAN_POINT('Ctrl Pts',(-0.354683465462343,3.22695369915506,
10.1993440059964));
#72041=CARTESIAN_POINT('Ctrl Pts',(-2.89518070317902,1.4686589914253,10.3572051171075));
#72042=CARTESIAN_POINT('Ctrl Pts',(-2.81336813298999,-1.61987353998757,
10.5150662282186));
#72043=CARTESIAN_POINT('Ctrl Pts',(-0.183347487058001,-3.24120567629433,
10.6729273393297));
#72044=CARTESIAN_POINT('Ctrl Pts',(2.61274013797703,-1.9268158989588,10.8307884504409));
#72045=CARTESIAN_POINT('Ctrl Pts',(3.04233848605292,1.13278730312457,10.988649561552));
#72046=CARTESIAN_POINT('Ctrl Pts',(0.716338869857416,3.16636844976869,11.1465106726631));
#72047=CARTESIAN_POINT('Ctrl Pts',(-2.25848464894066,2.33201149812516,11.3043717837742));
#72048=CARTESIAN_POINT('Ctrl Pts',(-3.18768578696123,-0.61456477697643,
11.4622328948853));
#72049=CARTESIAN_POINT('Ctrl Pts',(-1.22964064685199,-3.00449902792679,
11.6200940059964));
#72050=CARTESIAN_POINT('Ctrl Pts',(1.84215145675955,-2.67310840566659,11.7779551171075));
#72051=CARTESIAN_POINT('Ctrl Pts',(3.24541495852771,0.0794500556270124,
11.9358162282186));
#72052=CARTESIAN_POINT('Ctrl Pts',(1.70914397486321,2.76004662101762,12.0936773393297));
#72053=CARTESIAN_POINT('Ctrl Pts',(-1.37518406902836,2.94073108937221,12.2515384504409));
#72054=CARTESIAN_POINT('Ctrl Pts',(-3.21393924949186,0.457848448617044,
12.409399561552));
#72055=CARTESIAN_POINT('Ctrl Pts',(-2.14166898008542,-2.43973032873338,
12.5672606726631));
#72056=CARTESIAN_POINT('Ctrl Pts',(0.870417690451563,-3.12752360534598,
12.7251217837742));
#72057=CARTESIAN_POINT('Ctrl Pts',(3.09412394134766,-0.98256221591188,12.8829828948853));
#72058=CARTESIAN_POINT('Ctrl Pts',(2.51532684882466,2.05235432006483,13.0408440059964));
#72059=CARTESIAN_POINT('Ctrl Pts',(-0.341726090504644,3.22835204655998,
13.1987051171075));
#72060=CARTESIAN_POINT('Ctrl Pts',(-2.88926321104715,1.48026805649486,13.3565662282186));
#72061=CARTESIAN_POINT('Ctrl Pts',(-2.81984537414356,-1.60856488971291,
13.5144273393297));
#72062=CARTESIAN_POINT('Ctrl Pts',(-0.196362095487134,-3.24044746735677,
13.6722884504409));
#72063=CARTESIAN_POINT('Ctrl Pts',(2.60499409125458,-1.93728109181189,13.830149561552));
#72064=CARTESIAN_POINT('Ctrl Pts',(3.04684269509828,1.12055121749295,13.9880106726631));
#72065=CARTESIAN_POINT('Ctrl Pts',(0.729079149865556,3.16349462314833,14.1458717837742));
#72066=CARTESIAN_POINT('Ctrl Pts',(-2.24917294156805,2.34100677226896,14.3037328948853));
#72067=CARTESIAN_POINT('Ctrl Pts',(-3.1899976678388,-0.601664229474863,
14.4615940059964));
#72068=CARTESIAN_POINT('Ctrl Pts',(-1.24193888437236,-2.9997287294955,14.6194551171075));
#72069=CARTESIAN_POINT('Ctrl Pts',(1.83187902672385,-2.68011856729716,14.7773162282186));
#72070=CARTESIAN_POINT('Ctrl Pts',(3.24480068919561,0.0657260169420378,
14.9351773393297));
#72071=CARTESIAN_POINT('Ctrl Pts',(1.72197422097186,2.75450759860113,15.0930384504409));
#72072=CARTESIAN_POINT('Ctrl Pts',(-1.36701844957144,2.94352269819615,15.250899561552));
#72073=CARTESIAN_POINT('Ctrl Pts',(-2.59089728316432,1.29927701587847,15.3561403022927));
#72074=CARTESIAN_POINT('Ctrl Pts',(-2.72283095673204,0.399045011670964,
15.4087606726631));
#72075=CARTESIAN_POINT('Ctrl Pts',(1.48738611075532,-2.0858265952159,-0.109744663668465));
#72076=CARTESIAN_POINT('Ctrl Pts',(2.17700947925639,-1.59406173695134,-0.0571242932980945));
#72077=CARTESIAN_POINT('Ctrl Pts',(3.01897742315769,0.118289920962009,0.0481164474426461));
#72078=CARTESIAN_POINT('Ctrl Pts',(1.5499915516876,2.59665020929587,0.205977558553758));
#72079=CARTESIAN_POINT('Ctrl Pts',(-1.32417750849926,2.71565076394683,0.363838669664868));
#72080=CARTESIAN_POINT('Ctrl Pts',(-2.99830059390304,0.37867490595458,0.521699780775981));
#72081=CARTESIAN_POINT('Ctrl Pts',(-1.95706531655079,-2.30321564229053,
0.679560891887089));
#72082=CARTESIAN_POINT('Ctrl Pts',(0.856966242215927,-2.89796069680035,
0.837422002998203));
#72083=CARTESIAN_POINT('Ctrl Pts',(2.89470410572683,-0.86840536622856,0.995283114109312));
#72084=CARTESIAN_POINT('Ctrl Pts',(2.31061438218297,1.94798413339166,1.15314422522042));
#72085=CARTESIAN_POINT('Ctrl Pts',(-0.36634068394286,2.99984258826965,1.31100533633153));
#72086=CARTESIAN_POINT('Ctrl Pts',(-2.71146884103322,1.33466937183879,1.46886644744265));
#72087=CARTESIAN_POINT('Ctrl Pts',(-2.60069145140856,-1.53942016697539,
1.62672755855376));
#72088=CARTESIAN_POINT('Ctrl Pts',(-0.134334087372704,-3.01915922588007,
1.78458866966487));
#72089=CARTESIAN_POINT('Ctrl Pts',(2.45369438467058,-1.76430578301097,1.94244978077598));
#72090=CARTESIAN_POINT('Ctrl Pts',(2.81929030415377,1.0885732319059,2.10031089188709));
#72091=CARTESIAN_POINT('Ctrl Pts',(0.63131359737191,2.95547411242131,2.2581720029982));
#72092=CARTESIAN_POINT('Ctrl Pts',(-2.12847509047765,2.14545598790649,2.41603311410931));
#72093=CARTESIAN_POINT('Ctrl Pts',(-2.96039769805142,-0.607809627659522,
2.57389422522043));
#72094=CARTESIAN_POINT('Ctrl Pts',(-1.11094012909538,-2.81055127056503,
2.73175533633153));
#72095=CARTESIAN_POINT('Ctrl Pts',(1.74475137719111,-2.46763643396825,2.88961644744264));
#72096=CARTESIAN_POINT('Ctrl Pts',(3.02013441366314,0.110340122368272,3.04747755855376));
#72097=CARTESIAN_POINT('Ctrl Pts',(1.56003081265866,2.58837605606472,3.20533866966487));
#72098=CARTESIAN_POINT('Ctrl Pts',(-1.31307062963587,2.72199051088731,3.36319978077598));
#72099=CARTESIAN_POINT('Ctrl Pts',(-2.99685840389804,0.390162150876873,
3.52106089188709));
#72100=CARTESIAN_POINT('Ctrl Pts',(-1.96624179520275,-2.29505555316004,
3.6789220029982));
#72101=CARTESIAN_POINT('Ctrl Pts',(0.845298241250599,-2.90152678486402,
3.83678311410932));
#72102=CARTESIAN_POINT('Ctrl Pts',(2.89120942940861,-0.879940243000373,
3.99464422522043));
#72103=CARTESIAN_POINT('Ctrl Pts',(2.31840779046938,1.93865213806179,4.15250533633154));
#72104=CARTESIAN_POINT('Ctrl Pts',(-0.354291613296782,3.00131042205302,
4.31036644744265));
#72105=CARTESIAN_POINT('Ctrl Pts',(-2.70609140233011,1.34553190907942,4.46822755855376));
#72106=CARTESIAN_POINT('Ctrl Pts',(-2.60684901020221,-1.52896207739209,
4.62608866966487));
#72107=CARTESIAN_POINT('Ctrl Pts',(-0.146453229726317,-3.01859872255171,
4.78394978077598));
#72108=CARTESIAN_POINT('Ctrl Pts',(2.44659255781772,-1.77413969354566,4.94181089188709));
#72109=CARTESIAN_POINT('Ctrl Pts',(2.82363723243009,1.07724629301989,5.09967200299821));
#72110=CARTESIAN_POINT('Ctrl Pts',(0.643172594931182,2.95291649210482,5.25753311410931));
#72111=CARTESIAN_POINT('Ctrl Pts',(-2.11984559510778,2.15398269470792,5.41539422522043));
#72112=CARTESIAN_POINT('Ctrl Pts',(-2.96281372083041,-0.595920843619846,
5.57325533633153));
#72113=CARTESIAN_POINT('Ctrl Pts',(-1.12221343555009,-2.80606910130085,
5.73111644744265));
#72114=CARTESIAN_POINT('Ctrl Pts',(1.73483162480106,-2.47462038094578,5.88897755855376));
#72115=CARTESIAN_POINT('Ctrl Pts',(3.02055300928471,0.0982156520305535,
6.04683866966487));
#72116=CARTESIAN_POINT('Ctrl Pts',(1.57040862452068,2.58209286204701,6.20469978077598));
#72117=CARTESIAN_POINT('Ctrl Pts',(-1.30213331007977,2.72723956391501,6.36256089188709));
#72118=CARTESIAN_POINT('Ctrl Pts',(-2.99526805033731,0.402189138131933,
6.52042200299821));
#72119=CARTESIAN_POINT('Ctrl Pts',(-1.97543887191833,-2.28714408368097,
6.67828311410931));
#72120=CARTESIAN_POINT('Ctrl Pts',(0.833643986972413,-2.90489664173917,
6.83614422522043));
#72121=CARTESIAN_POINT('Ctrl Pts',(2.88765383748144,-0.891539180900916,
6.99400533633154));
#72122=CARTESIAN_POINT('Ctrl Pts',(2.32617133837164,1.9293298579406,7.15186644744265));
#72123=CARTESIAN_POINT('Ctrl Pts',(-0.342240758892514,3.00270845390548,
7.30972755855377));
#72124=CARTESIAN_POINT('Ctrl Pts',(-2.70066830226297,1.35638398595488,7.46758866966487));
#72125=CARTESIAN_POINT('Ctrl Pts',(-2.61296563717754,-1.51848522387679,
7.62544978077598));
#72126=CARTESIAN_POINT('Ctrl Pts',(-0.158569449084724,-3.01798650196116,
7.78331089188708));
#72127=CARTESIAN_POINT('Ctrl Pts',(2.43945101127409,-1.78394662470507,7.94117200299821));
#72128=CARTESIAN_POINT('Ctrl Pts',(2.8279388142067,1.06590283764795,8.09903311410931));
#72129=CARTESIAN_POINT('Ctrl Pts',(0.655021147500741,2.95031084676337,8.25689422522044));
#72130=CARTESIAN_POINT('Ctrl Pts',(-2.11118189776743,2.16247492256949,8.41475533633153));
#72131=CARTESIAN_POINT('Ctrl Pts',(-2.96518202224487,-0.584022577610279,
8.57261644744266));
#72132=CARTESIAN_POINT('Ctrl Pts',(-1.13346864680612,-2.8015416511111,8.73047755855375));
#72133=CARTESIAN_POINT('Ctrl Pts',(1.72488391085535,-2.48156448440799,8.88833866966489));
#72134=CARTESIAN_POINT('Ctrl Pts',(3.0209229341641,0.0860896163543999,9.04619978077597));
#72135=CARTESIAN_POINT('Ctrl Pts',(1.58076112878023,2.575768050493,9.2040608918871));
#72136=CARTESIAN_POINT('Ctrl Pts',(-1.2911750067657,2.73244467429924,9.3619220029982));
#72137=CARTESIAN_POINT('Ctrl Pts',(-2.99362943076381,0.414209641928883,
9.51978311410932));
#72138=CARTESIAN_POINT('Ctrl Pts',(-1.98460411570002,-2.27919575731244,
9.67764422522042));
#72139=CARTESIAN_POINT('Ctrl Pts',(0.821976299030791,-2.90821968909385,
9.83550533633154));
#72140=CARTESIAN_POINT('Ctrl Pts',(2.88405171327213,-0.903123751969326,
9.99336644744264));
#72141=CARTESIAN_POINT('Ctrl Pts',(2.33389740175841,1.9199764879499,10.1512275585538));
#72142=CARTESIAN_POINT('Ctrl Pts',(-0.330184389523787,3.00405809948898,
10.3090886696649));
#72143=CARTESIAN_POINT('Ctrl Pts',(-2.69520168298246,1.36721420568682,10.466949780776));
#72144=CARTESIAN_POINT('Ctrl Pts',(-2.61904015820422,-1.50798390110827,
10.6248108918871));
#72145=CARTESIAN_POINT('Ctrl Pts',(-0.170683113197963,-3.01732564880962,
10.7826720029982));
#72146=CARTESIAN_POINT('Ctrl Pts',(2.43227015479182,-1.793724808945,10.9405331141093));
#72147=CARTESIAN_POINT('Ctrl Pts',(2.83219482597701,1.05454220611865,11.0983942252204));
#72148=CARTESIAN_POINT('Ctrl Pts',(0.666859144752323,2.94765765929168,11.2562553363315));
#72149=CARTESIAN_POINT('Ctrl Pts',(-2.10248418004828,2.17093230401124,11.4141164474427));
#72150=CARTESIAN_POINT('Ctrl Pts',(-2.96750254255404,-0.572114900942073,
11.5719775585538));
#72151=CARTESIAN_POINT('Ctrl Pts',(-1.14470559202747,-2.79696905540156,
11.7298386696649));
#72152=CARTESIAN_POINT('Ctrl Pts',(1.7149083997124,-2.48846860088429,11.887699780776));
#72153=CARTESIAN_POINT('Ctrl Pts',(3.02124418299545,0.0739621963506113,
12.0455608918871));
#72154=CARTESIAN_POINT('Ctrl Pts',(1.5910881529614,2.56940172677601,12.2034220029982));
#72155=CARTESIAN_POINT('Ctrl Pts',(-1.28019588317448,2.73760576414863,12.3612831141093));
#72156=CARTESIAN_POINT('Ctrl Pts',(-2.99194259782208,0.42622345054612,12.5191442252204));
#72157=CARTESIAN_POINT('Ctrl Pts',(-1.99373732809816,-2.27121066426194,
12.6770053363315));
#72158=CARTESIAN_POINT('Ctrl Pts',(0.810295268142284,-2.91149594753796,
12.8348664474426));
#72159=CARTESIAN_POINT('Ctrl Pts',(2.88040330087848,-0.914693626913434,
12.9927275585538));
#72160=CARTESIAN_POINT('Ctrl Pts',(2.34158550060768,1.91059190586663,13.1505886696649));
#72161=CARTESIAN_POINT('Ctrl Pts',(-0.318122020237242,3.00535985874532,
13.308449780776));
#72162=CARTESIAN_POINT('Ctrl Pts',(-2.68969293020052,1.37802139698889,13.4663108918871));
#72163=CARTESIAN_POINT('Ctrl Pts',(-2.62506999642434,-1.49745637402886,
13.6241720029982));
#72164=CARTESIAN_POINT('Ctrl Pts',(-0.182798762664348,-3.0166198116913,
13.7820331141093));
#72165=CARTESIAN_POINT('Ctrl Pts',(2.42505915129906,-1.80346713879661,13.9398942252204));
#72166=CARTESIAN_POINT('Ctrl Pts',(2.8363879154744,1.04315130448987,14.0977553363316));
#72167=CARTESIAN_POINT('Ctrl Pts',(0.678719414504022,2.94498233669946,14.2556164474426));
#72168=CARTESIAN_POINT('Ctrl Pts',(-2.09381566089348,2.17930624695187,14.4134775585538));
#72169=CARTESIAN_POINT('Ctrl Pts',(-2.96965473472126,-0.560105433864789,
14.5713386696649));
#72170=CARTESIAN_POINT('Ctrl Pts',(-1.15615435252323,-2.79252825612909,
14.729199780776));
#72171=CARTESIAN_POINT('Ctrl Pts',(1.70534551795855,-2.49499454912784,14.8870608918871));
#72172=CARTESIAN_POINT('Ctrl Pts',(3.0206723431321,0.0611861191543108,15.0449220029982));
#72173=CARTESIAN_POINT('Ctrl Pts',(1.60303217457882,2.56424530164419,15.2027831141093));
#72174=CARTESIAN_POINT('Ctrl Pts',(-1.27259428812422,2.74020454798006,15.3606442252204));
#72175=CARTESIAN_POINT('Ctrl Pts',(-2.41193605302479,1.20953196324185,15.4658849659612));
#72176=CARTESIAN_POINT('Ctrl Pts',(-2.53475666268529,0.371481747533179,
15.5185053363315));
#72177=CARTESIAN_POINT('Ctrl Pts',(1.37702479013102,-1.93106208855765,-3.60822483003176E-15));
#72178=CARTESIAN_POINT('Ctrl Pts',(2.01547936988864,-1.47578528057288,0.0526203703703667));
#72179=CARTESIAN_POINT('Ctrl Pts',(2.79497483704674,0.109513025844136,0.157861111111108));
#72180=CARTESIAN_POINT('Ctrl Pts',(1.4349850222035,2.40398352764199,0.315722222222219));
#72181=CARTESIAN_POINT('Ctrl Pts',(-1.225925966736,2.51415445945906,0.473583333333329));
#72182=CARTESIAN_POINT('Ctrl Pts',(-2.77583219058859,0.350577922658662,
0.631444444444441));
#72183=CARTESIAN_POINT('Ctrl Pts',(-1.811854660541,-2.13232126716645,0.789305555555552));
#72184=CARTESIAN_POINT('Ctrl Pts',(0.793380919254056,-2.68293732976497,
0.947166666666663));
#72185=CARTESIAN_POINT('Ctrl Pts',(2.67992237177449,-0.803971281251394,
1.10502777777777));
#72186=CARTESIAN_POINT('Ctrl Pts',(2.13917103413275,1.80344728451176,1.26288888888888));
#72187=CARTESIAN_POINT('Ctrl Pts',(-0.339158877291603,2.77725977180218,
1.42075));
#72188=CARTESIAN_POINT('Ctrl Pts',(-2.51028282755341,1.23563935306431,1.57861111111111));
#72189=CARTESIAN_POINT('Ctrl Pts',(-2.40772491700405,-1.42519801484247,
1.73647222222222));
#72190=CARTESIAN_POINT('Ctrl Pts',(-0.124366744542119,-2.79514315034066,
1.89433333333333));
#72191=CARTESIAN_POINT('Ctrl Pts',(2.27163476293377,-1.63339753074864,2.05219444444444));
#72192=CARTESIAN_POINT('Ctrl Pts',(2.61010413592219,1.00780309522069,2.21005555555555));
#72193=CARTESIAN_POINT('Ctrl Pts',(0.584471286669745,2.73618335546233,2.36791666666667));
#72194=CARTESIAN_POINT('Ctrl Pts',(-1.97054614371495,1.98626708970809,2.52577777777777));
#72195=CARTESIAN_POINT('Ctrl Pts',(-2.7407416200716,-0.562711268389121,
2.68363888888889));
#72196=CARTESIAN_POINT('Ctrl Pts',(-1.02851040967351,-2.60201352259292,
2.84149999999999));
#72197=CARTESIAN_POINT('Ctrl Pts',(1.61529402596567,-2.28454233775194,2.99936111111111));
#72198=CARTESIAN_POINT('Ctrl Pts',(2.79604598097933,0.102153087721166,3.15722222222222));
#72199=CARTESIAN_POINT('Ctrl Pts',(1.44427938842878,2.39632330140064,3.31508333333333));
#72200=CARTESIAN_POINT('Ctrl Pts',(-1.21564319790733,2.5200238088076,3.47294444444445));
#72201=CARTESIAN_POINT('Ctrl Pts',(-2.77449700843608,0.361212835082494,
3.63080555555555));
#72202=CARTESIAN_POINT('Ctrl Pts',(-1.82035026131238,-2.12476664167876,
3.78866666666667));
#72203=CARTESIAN_POINT('Ctrl Pts',(0.782578662553965,-2.68623882063674,
3.94652777777777));
#72204=CARTESIAN_POINT('Ctrl Pts',(2.67668699402767,-0.814650291328897,
4.10438888888889));
#72205=CARTESIAN_POINT('Ctrl Pts',(2.14638618582228,1.79480770611467,4.26225));
#72206=CARTESIAN_POINT('Ctrl Pts',(-0.328003825581952,2.77861869501174,
4.42011111111111));
#72207=CARTESIAN_POINT('Ctrl Pts',(-2.50530438493649,1.24569590997036,4.57797222222222));
#72208=CARTESIAN_POINT('Ctrl Pts',(-2.41342559623202,-1.41551589631959,
4.73583333333333));
#72209=CARTESIAN_POINT('Ctrl Pts',(-0.135586668767159,-2.79462423533096,
4.89369444444444));
#72210=CARTESIAN_POINT('Ctrl Pts',(2.2650598786042,-1.64250178316317,5.05155555555556));
#72211=CARTESIAN_POINT('Ctrl Pts',(2.61412853009539,0.997316594419356,5.20941666666666));
#72212=CARTESIAN_POINT('Ctrl Pts',(0.595450368366912,2.73381550588105,5.36727777777778));
#72213=CARTESIAN_POINT('Ctrl Pts',(-1.96255694106964,1.99416113050815,5.52513888888888));
#72214=CARTESIAN_POINT('Ctrl Pts',(-2.74297837839289,-0.551704610313744,
5.683));
#72215=CARTESIAN_POINT('Ctrl Pts',(-1.03894725747156,-2.59786392206505,
5.84086111111111));
#72216=CARTESIAN_POINT('Ctrl Pts',(1.60611030100396,-2.29100808867664,5.99872222222222));
#72217=CARTESIAN_POINT('Ctrl Pts',(2.79643351757374,0.090928230838667,6.15658333333333));
#72218=CARTESIAN_POINT('Ctrl Pts',(1.45388718569001,2.39050630885174,6.31444444444444));
#72219=CARTESIAN_POINT('Ctrl Pts',(-1.20551740739643,2.52488339173069,6.47230555555556));
#72220=CARTESIAN_POINT('Ctrl Pts',(-2.77302465619186,0.372347441948222,
6.63016666666666));
#72221=CARTESIAN_POINT('Ctrl Pts',(-1.82886493180883,-2.11744218872047,
6.78802777777778));
#72222=CARTESIAN_POINT('Ctrl Pts',(0.771789132562049,-2.68935864031417,
6.94588888888888));
#72223=CARTESIAN_POINT('Ctrl Pts',(2.67339522049833,-0.825388609316905,
7.10375));
#72224=CARTESIAN_POINT('Ctrl Pts',(2.15357369271338,1.7861771220756,7.26161111111111));
#72225=CARTESIAN_POINT('Ctrl Pts',(-0.3168471224657,2.77991299546561,7.41947222222222));
#72226=CARTESIAN_POINT('Ctrl Pts',(-2.50028366894498,1.25574278265114,7.57733333333334));
#72227=CARTESIAN_POINT('Ctrl Pts',(-2.41908838070749,-1.40581640611404,
7.73519444444443));
#72228=CARTESIAN_POINT('Ctrl Pts',(-0.146803886877873,-2.79405744038503,
7.89305555555557));
#72229=CARTESIAN_POINT('Ctrl Pts',(2.25844822171206,-1.65158105802259,8.05091666666665));
#72230=CARTESIAN_POINT('Ctrl Pts',(2.61811094239596,0.986814802625037,8.20877777777778));
#72231=CARTESIAN_POINT('Ctrl Pts',(0.606419780073446,2.73140319464357,8.36663888888888));
#72232=CARTESIAN_POINT('Ctrl Pts',(-1.95453607417732,2.00202325064244,8.52450000000001));
#72233=CARTESIAN_POINT('Ctrl Pts',(-2.74517095618734,-0.540689173813247,
8.68236111111111));
#72234=CARTESIAN_POINT('Ctrl Pts',(-1.04936735270146,-2.59367240037321,
8.84022222222223));
#72235=CARTESIAN_POINT('Ctrl Pts',(1.59690068918271,-2.29743695240177,8.99808333333332));
#72236=CARTESIAN_POINT('Ctrl Pts',(2.79677599470576,0.0797019247629725,
9.15594444444445));
#72237=CARTESIAN_POINT('Ctrl Pts',(1.46347155312646,2.38465078671139,9.31380555555555));
#72238=CARTESIAN_POINT('Ctrl Pts',(-1.19537219008389,2.52970229247383,9.47166666666666));
#72239=CARTESIAN_POINT('Ctrl Pts',(-2.77150761918447,0.383476046416537,
9.62952777777778));
#72240=CARTESIAN_POINT('Ctrl Pts',(-1.83735013131669,-2.1100836135863,9.78738888888888));
#72241=CARTESIAN_POINT('Ctrl Pts',(0.760987165659879,-2.69243512365168,
9.94525));
#72242=CARTESIAN_POINT('Ctrl Pts',(2.6700603672968,-0.836113626465368,10.1031111111111));
#72243=CARTESIAN_POINT('Ctrl Pts',(2.16072649637127,1.7775177549783,10.2609722222222));
#72244=CARTESIAN_POINT('Ctrl Pts',(-0.305685313585232,2.78116249982291,
10.4188333333333));
#72245=CARTESIAN_POINT('Ctrl Pts',(-2.4952226627859,1.26576941994835,10.5766944444444));
#72246=CARTESIAN_POINT('Ctrl Pts',(-2.42471218341845,-1.39609426222898,
10.7345555555556));
#72247=CARTESIAN_POINT('Ctrl Pts',(-0.158018739337926,-2.79344562132492,
10.8924166666667));
#72248=CARTESIAN_POINT('Ctrl Pts',(2.25180017160661,-1.66063371893121,11.0502777777778));
#72249=CARTESIAN_POINT('Ctrl Pts',(2.62205116590109,0.976297109112734,11.2081388888889));
#72250=CARTESIAN_POINT('Ctrl Pts',(0.617379419647229,2.72894686881467,11.366));
#72251=CARTESIAN_POINT('Ctrl Pts',(-1.9464837111559,2.00985310989732,11.5238611111111));
#72252=CARTESIAN_POINT('Ctrl Pts',(-2.74731929814685,-0.529665024907718,
11.6817222222222));
#72253=CARTESIAN_POINT('Ctrl Pts',(-1.05977053720295,-2.58943908287633,
11.8395833333333));
#72254=CARTESIAN_POINT('Ctrl Pts',(1.58766534266525,-2.30382879610199,11.9974444444444));
#72255=CARTESIAN_POINT('Ctrl Pts',(2.79707340746319,0.0684743370742143,
12.1553055555555));
#72256=CARTESIAN_POINT('Ctrl Pts',(1.47303233105958,2.37875683253439,12.3131666666667));
#72257=CARTESIAN_POINT('Ctrl Pts',(-1.18520769732058,2.53448043892505,12.4710277777778));
#72258=CARTESIAN_POINT('Ctrl Pts',(-2.76994594615232,0.394598452475193,
12.6288888888889));
#72259=CARTESIAN_POINT('Ctrl Pts',(-1.8458056761109,-2.1026909997905,12.78675));
#72260=CARTESIAN_POINT('Ctrl Pts',(0.750172845833004,-2.69546828972993,
12.9446111111111));
#72261=CARTESIAN_POINT('Ctrl Pts',(2.66668266040929,-0.846825037914988,
13.1024722222222));
#72262=CARTESIAN_POINT('Ctrl Pts',(2.16784415239069,1.76882949166842,13.2603333333333));
#72263=CARTESIAN_POINT('Ctrl Pts',(-0.294517949969841,2.78236767093066,
13.4181944444444));
#72264=CARTESIAN_POINT('Ctrl Pts',(-2.49012264935389,1.27577473748293,13.5760555555556));
#72265=CARTESIAN_POINT('Ctrl Pts',(-2.43029461870512,-1.3863478583448,13.7339166666666));
#72266=CARTESIAN_POINT('Ctrl Pts',(-0.16923542984156,-2.79279215602584,
13.8917777777778));
#72267=CARTESIAN_POINT('Ctrl Pts',(2.24512421134353,-1.66965318578134,14.0496388888889));
#72268=CARTESIAN_POINT('Ctrl Pts',(2.62593313585052,0.965751391486786,14.2075));
#72269=CARTESIAN_POINT('Ctrl Pts',(0.628359679142483,2.72647005025058,14.3653611111111));
#72270=CARTESIAN_POINT('Ctrl Pts',(-1.93845838021891,2.01760572163479,14.5232222222222));
#72271=CARTESIAN_POINT('Ctrl Pts',(-2.74931180160372,-0.518546638254714,
14.6810833333333));
#72272=CARTESIAN_POINT('Ctrl Pts',(-1.07036982067409,-2.58532778276268,
14.8389444444444));
#72273=CARTESIAN_POINT('Ctrl Pts',(1.57881200919325,-2.30987053095853,14.9968055555556));
#72274=CARTESIAN_POINT('Ctrl Pts',(2.79654399706859,0.0566462213665858,
15.1546666666667));
#72275=CARTESIAN_POINT('Ctrl Pts',(1.48409012818578,2.37398300468726,15.3125277777778));
#72276=CARTESIAN_POINT('Ctrl Pts',(-1.17817012667699,2.53688639776398,15.4703888888889));
#72277=CARTESIAN_POINT('Ctrl Pts',(-2.23297482288527,1.11978691060522,15.5756296296296));
#72278=CARTESIAN_POINT('Ctrl Pts',(-2.34668236863854,0.343918483395395,
15.62825));
#72279=CARTESIAN_POINT('',(1.37702479013102,-1.93106208855765,0.));
#72280=CARTESIAN_POINT('Ctrl Pts',(1.37702479013102,-1.93106208855765,-3.60822483003176E-15));
#72281=CARTESIAN_POINT('Ctrl Pts',(2.01547936988864,-1.47578528057288,0.0526203703703667));
#72282=CARTESIAN_POINT('Ctrl Pts',(2.79497483704674,0.109513025844136,0.157861111111108));
#72283=CARTESIAN_POINT('Ctrl Pts',(1.4349850222035,2.40398352764199,0.315722222222219));
#72284=CARTESIAN_POINT('Ctrl Pts',(-1.225925966736,2.51415445945906,0.473583333333329));
#72285=CARTESIAN_POINT('Ctrl Pts',(-2.32453883371355,0.980556500150706,
0.585479295290919));
#72286=CARTESIAN_POINT('Ctrl Pts',(-2.37485146083742,0.100616720091163,
0.644754886878137));
#72287=CARTESIAN_POINT('Ctrl Pts',(-2.37409249406917,0.00172857025301858,
0.651410108094986));
#72288=CARTESIAN_POINT('Ctrl Pts',(1.29200104020317,2.64812001020929,8.84708972748172E-17));
#72289=CARTESIAN_POINT('Ctrl Pts',(1.36315737313149,2.60529414881161,1.11522009070411E-16));
#72290=CARTESIAN_POINT('Ctrl Pts',(1.43224767624703,2.55934891308958,-5.0435019692162E-16));
#72291=CARTESIAN_POINT('Ctrl Pts',(1.49903325513988,2.51027466650741,-4.38885039422132E-16));
#72292=CARTESIAN_POINT('Ctrl Pts',(1.57786836962904,2.45234638450537,-3.65724347932505E-16));
#72293=CARTESIAN_POINT('Ctrl Pts',(1.65349331585608,2.39005818913334,-5.19266877679362E-16));
#72294=CARTESIAN_POINT('Ctrl Pts',(1.72573019513852,2.32378926839401,-6.48786580015326E-16));
#72295=CARTESIAN_POINT('Ctrl Pts',(1.76374109312884,2.28891869797108,-7.16939582223243E-16));
#72296=CARTESIAN_POINT('Ctrl Pts',(1.80081318017132,2.2529453987339,-5.63901193634668E-16));
#72297=CARTESIAN_POINT('Ctrl Pts',(1.83691551656788,2.21592189026143,-5.759281940243E-16));
#72298=CARTESIAN_POINT('Ctrl Pts',(1.85077163488616,2.20171222503873,-5.80544170635404E-16));
#72299=CARTESIAN_POINT('Ctrl Pts',(1.86448486767998,2.18734784556943,1.18680337545582E-16));
#72300=CARTESIAN_POINT('Ctrl Pts',(1.87805332095389,2.17283167229843,1.45716771982052E-16));
#72301=CARTESIAN_POINT('Ctrl Pts',(1.88973877018296,2.16033002584437,1.69001141656681E-16));
#72302=CARTESIAN_POINT('Ctrl Pts',(1.90131548250979,2.14771713833219,-1.20552840767492E-16));
#72303=CARTESIAN_POINT('Ctrl Pts',(1.91277473204616,2.1350036118777,-1.04083408558608E-16));
#72304=CARTESIAN_POINT('Ctrl Pts',(1.9778462733255,2.06280963801715,-1.05614606835039E-17));
#72305=CARTESIAN_POINT('Ctrl Pts',(2.03920496551099,1.98729716595704,-4.81412066085989E-16));
#72306=CARTESIAN_POINT('Ctrl Pts',(2.09668120715734,1.90884345828848,-3.33066907387547E-16));
#72307=CARTESIAN_POINT('Ctrl Pts',(2.14417843271961,1.84401087107344,-2.10477411937863E-16));
#72308=CARTESIAN_POINT('Ctrl Pts',(2.18902362087598,1.7771688452355,-1.7119245770294E-16));
#72309=CARTESIAN_POINT('Ctrl Pts',(2.23109606376114,1.7085204430367,-1.94289029309402E-16));
#72310=CARTESIAN_POINT('Ctrl Pts',(2.24950275752339,1.67848676707472,-2.0439377938723E-16));
#72311=CARTESIAN_POINT('Ctrl Pts',(2.26737842523222,1.6481072631063,-4.61788465798711E-16));
#72312=CARTESIAN_POINT('Ctrl Pts',(2.28471149018554,1.61739870311764,-5.13478148889135E-16));
#72313=CARTESIAN_POINT('Ctrl Pts',(2.29518347047447,1.59884575614786,-5.44707094486553E-16));
#72314=CARTESIAN_POINT('Ctrl Pts',(2.30545737670969,1.58017269818218,-5.13081578012294E-16));
#72315=CARTESIAN_POINT('Ctrl Pts',(2.3155304906665,1.56138322284078,-5.55111512312578E-16));
#72316=CARTESIAN_POINT('Ctrl Pts',(2.32274660107223,1.54792294341672,-5.85220637212436E-16));
#72317=CARTESIAN_POINT('Ctrl Pts',(2.32985933504635,1.5344033850802,-2.08590721469464E-17));
#72318=CARTESIAN_POINT('Ctrl Pts',(2.33686168047272,1.52083799385098,-2.77555756156289E-17));
#72319=CARTESIAN_POINT('Ctrl Pts',(2.38047027627073,1.43635663411551,-7.07050181056999E-17));
#72320=CARTESIAN_POINT('Ctrl Pts',(2.41986655819018,1.34997905359849,1.3198210981114E-16));
#72321=CARTESIAN_POINT('Ctrl Pts',(2.45488985599288,1.26205357875123,5.55111512312578E-17));
#72322=CARTESIAN_POINT('Ctrl Pts',(2.48959846523414,1.17491812491653,-2.02727065483809E-17));
#72323=CARTESIAN_POINT('Ctrl Pts',(2.52001253380174,1.08626153918075,-4.44579204063227E-16));
#72324=CARTESIAN_POINT('Ctrl Pts',(2.54592562425351,0.996413712953991,-4.9960036108132E-16));
#72325=CARTESIAN_POINT('Ctrl Pts',(2.57101139534936,0.909434430942866,-5.528648743571E-16));
#72326=CARTESIAN_POINT('Ctrl Pts',(2.59187898968551,0.821337996875181,-7.89241560757653E-18));
#72327=CARTESIAN_POINT('Ctrl Pts',(2.60829286172102,0.732427405689614,-8.32667268468867E-17));
#72328=CARTESIAN_POINT('Ctrl Pts',(2.61783087340729,0.680761945161682,-1.27066328786625E-16));
#72329=CARTESIAN_POINT('Ctrl Pts',(2.62586408863254,0.628821695636964,-4.14952786105416E-17));
#72330=CARTESIAN_POINT('Ctrl Pts',(2.63233843305125,0.576668196894126,-5.55111512312578E-17));
#72331=CARTESIAN_POINT('Ctrl Pts',(2.63414224296016,0.562137768524485,-5.94160979378542E-17));
#72332=CARTESIAN_POINT('Ctrl Pts',(2.63582527555606,0.547588319420663,3.76279563716787E-16));
#72333=CARTESIAN_POINT('Ctrl Pts',(2.63738542604938,0.533029261526728,3.60822483003176E-16));
#72334=CARTESIAN_POINT('Ctrl Pts',(2.64690685377435,0.444176924476997,2.66489610960485E-16));
#72335=CARTESIAN_POINT('Ctrl Pts',(2.65183263786108,0.355196731300303,5.62349138697447E-16));
#72336=CARTESIAN_POINT('Ctrl Pts',(2.65198717743404,0.266381980286723,3.88578058618805E-16));
#72337=CARTESIAN_POINT('Ctrl Pts',(2.65207998114243,0.213047173573617,2.84225494854879E-16));
#72338=CARTESIAN_POINT('Ctrl Pts',(2.65045121279133,0.159772024909719,-3.854419951949E-17));
#72339=CARTESIAN_POINT('Ctrl Pts',(2.64705383408491,0.106621318043217,-8.32667268468867E-17));
#72340=CARTESIAN_POINT('Ctrl Pts',(2.64128166054733,0.0163178428672467,
-1.29468843946197E-16));
#72341=CARTESIAN_POINT('Ctrl Pts',(2.63040647827402,-0.0736278476965388,
-4.84995897836269E-16));
#72342=CARTESIAN_POINT('Ctrl Pts',(2.61462343406994,-0.162881882998066,
-6.10622663543836E-16));
#72343=CARTESIAN_POINT('Ctrl Pts',(2.59852152905154,-0.253939094797703,
-7.38787434739808E-16));
#72344=CARTESIAN_POINT('Ctrl Pts',(2.57731092756958,-0.344277415185344,
-3.0810955291451E-16));
#72345=CARTESIAN_POINT('Ctrl Pts',(2.55115372858487,-0.433510589178544,
-3.60822483003176E-16));
#72346=CARTESIAN_POINT('Ctrl Pts',(2.54730992415644,-0.446623417870874,
-3.68568656216471E-16));
#72347=CARTESIAN_POINT('Ctrl Pts',(2.54335838534963,-0.4597150170452,-1.33461876853334E-16));
#72348=CARTESIAN_POINT('Ctrl Pts',(2.53930241226215,-0.472774949708627,
-1.38777878078145E-16));
#72349=CARTESIAN_POINT('Ctrl Pts',(2.51300579541719,-0.557448106523011,
-1.73243798916645E-16));
#72350=CARTESIAN_POINT('Ctrl Pts',(2.48237490705721,-0.640633082262047,
2.2266366763076E-16));
#72351=CARTESIAN_POINT('Ctrl Pts',(2.4476284488952,-0.722031078376524,1.66533453693773E-16));
#72352=CARTESIAN_POINT('Ctrl Pts',(2.41285997251409,-0.803480654968775,
1.10367671027941E-16));
#72353=CARTESIAN_POINT('Ctrl Pts',(2.37397005509887,-0.883141781461701,
-2.60473824643759E-16));
#72354=CARTESIAN_POINT('Ctrl Pts',(2.33113438836321,-0.960686402199183,
-2.22044604925031E-16));
#72355=CARTESIAN_POINT('Ctrl Pts',(2.28891526223189,-1.03711491080453,-1.84168503113759E-16));
#72356=CARTESIAN_POINT('Ctrl Pts',(2.24286247138705,-1.11148803969701,-4.86311355035046E-16));
#72357=CARTESIAN_POINT('Ctrl Pts',(2.19311210725222,-1.18345333925267,-6.10622663543836E-16));
#72358=CARTESIAN_POINT('Ctrl Pts',(2.16658994742807,-1.22181838863071,-6.76893623556989E-16));
#72359=CARTESIAN_POINT('Ctrl Pts',(2.13901644812981,-1.25949841963374,-1.03661145615814E-16));
#72360=CARTESIAN_POINT('Ctrl Pts',(2.11040940583919,-1.29643454206688,-5.55111512312578E-17));
#72361=CARTESIAN_POINT('Ctrl Pts',(2.10166865720486,-1.30772020237512,-4.0799144537779E-17));
#72362=CARTESIAN_POINT('Ctrl Pts',(2.09283023898332,-1.31893783850973,-3.98702450321844E-16));
#72363=CARTESIAN_POINT('Ctrl Pts',(2.08389831377262,-1.33008110200649,-3.88578058618805E-16));
#72364=CARTESIAN_POINT('Ctrl Pts',(2.03043260129099,-1.39678368942974,-3.27974347428123E-16));
#72365=CARTESIAN_POINT('Ctrl Pts',(1.97380215986925,-1.46059813131217,-2.08556400160018E-16));
#72366=CARTESIAN_POINT('Ctrl Pts',(1.91417150281915,-1.52123259912064,-1.11022302462516E-16));
#72367=CARTESIAN_POINT('Ctrl Pts',(1.85542332105702,-1.58096973622562,-1.49316138302572E-17));
#72368=CARTESIAN_POINT('Ctrl Pts',(1.79376241718216,-1.63762085789259,-5.35520206863283E-16));
#72369=CARTESIAN_POINT('Ctrl Pts',(1.72931881925135,-1.69086532717403,-5.55111512312578E-16));
#72370=CARTESIAN_POINT('Ctrl Pts',(1.66690919772329,-1.7424292882658,-5.74084474679515E-16));
#72371=CARTESIAN_POINT('Ctrl Pts',(1.60188918190129,-1.79079854027645,-4.05239810717764E-16));
#72372=CARTESIAN_POINT('Ctrl Pts',(1.53436012060039,-1.83563678794726,-4.44089209850063E-16));
#72373=CARTESIAN_POINT('Ctrl Pts',(1.48333459704145,-1.8695169429323,-4.73444140786276E-16));
#72374=CARTESIAN_POINT('Ctrl Pts',(1.43087616732457,-1.90138023485661,-2.26823314612322E-16));
#72375=CARTESIAN_POINT('Ctrl Pts',(1.37702479013106,-1.93106208855762,-2.22044604925031E-16));
#72376=CARTESIAN_POINT('Ctrl Pts',(0.260984867623806,2.92515103163649,15.058));
#72377=CARTESIAN_POINT('Ctrl Pts',(0.721611965671866,2.88493263312463,15.0330979289241));
#72378=CARTESIAN_POINT('Ctrl Pts',(1.17298362662806,2.74202417939443,15.0081958578483));
#72379=CARTESIAN_POINT('Ctrl Pts',(1.56185858228333,2.49936439089571,14.9832937867724));
#72380=CARTESIAN_POINT('Ctrl Pts',(2.3835871899963,1.98660190194863,14.930673416402));
#72381=CARTESIAN_POINT('Ctrl Pts',(2.92625811262771,1.02843390833919,14.8780530460316));
#72382=CARTESIAN_POINT('Ctrl Pts',(2.94584082398175,0.0600984948350938,
14.8254326756613));
#72383=CARTESIAN_POINT('Ctrl Pts',(2.96542353533579,-0.90823691866899,14.7728123052909));
#72384=CARTESIAN_POINT('Ctrl Pts',(2.46191803541247,-1.88673975206773,14.7201919349205));
#72385=CARTESIAN_POINT('Ctrl Pts',(1.6624759601657,-2.43293893833301,14.6675715645502));
#72386=CARTESIAN_POINT('Ctrl Pts',(0.863033884918936,-2.97913812459828,
14.6149511941798));
#72387=CARTESIAN_POINT('Ctrl Pts',(-0.232344765651281,-3.0930336637301,
14.5623308238094));
#72388=CARTESIAN_POINT('Ctrl Pts',(-1.12713695505886,-2.72269707033318,
14.5097104534391));
#72389=CARTESIAN_POINT('Ctrl Pts',(-2.02192914446644,-2.35236047693625,
14.4570900830687));
#72390=CARTESIAN_POINT('Ctrl Pts',(-2.71613487271139,-1.49779175101059,
14.4044697126983));
#72391=CARTESIAN_POINT('Ctrl Pts',(-2.89560267371491,-0.546185667602603,
14.351849342328));
#72392=CARTESIAN_POINT('Ctrl Pts',(-2.9293373183321,-0.367311836977727,
14.3419582672485));
#72393=CARTESIAN_POINT('Ctrl Pts',(-2.94488478294563,-0.185009395803266,
14.3320671921691));
#72394=CARTESIAN_POINT('Ctrl Pts',(-2.94325266537063,-0.0024318079996577,
14.3221761170896));
#72395=CARTESIAN_POINT('Origin',(0.,0.,-1.84858989190501));
#72396=CARTESIAN_POINT('',(-1.37702479013098,-1.93106208855768,0.));
#72397=CARTESIAN_POINT('Ctrl Pts',(-1.37994859234593,-1.93347131995891,
-1.03866568124111E-15));
#72398=CARTESIAN_POINT('Ctrl Pts',(-0.794305021574331,-2.34617453422284,
0.0482502273315914));
#72399=CARTESIAN_POINT('Ctrl Pts',(0.853330802601401,-2.62819893329841,
0.149165418329868));
#72400=CARTESIAN_POINT('Ctrl Pts',(2.68321992772198,-0.795544356782894,
0.30274557299483));
#72401=CARTESIAN_POINT('Ctrl Pts',(2.13222685489998,1.81318819272267,0.460740463994884));
#72402=CARTESIAN_POINT('Ctrl Pts',(-0.353356050373597,2.77617865909866,
0.618735354994938));
#72403=CARTESIAN_POINT('Ctrl Pts',(-2.12480812784407,1.50378450145058,0.74801849763165));
#72404=CARTESIAN_POINT('Ctrl Pts',(-2.36883710346974,0.358840951777969,
0.824636676601679));
#72405=CARTESIAN_POINT('Ctrl Pts',(-2.36806791026422,0.000580996437929554,
0.848589891905023));
#72406=CARTESIAN_POINT('Origin',(0.,0.,0.));
#72407=CARTESIAN_POINT('Ctrl Pts',(-1.03908919352511,2.13201587949043,-0.329233991005384));
#72408=CARTESIAN_POINT('Ctrl Pts',(-1.74458119175558,1.78817739379635,-0.2765690273387));
#72409=CARTESIAN_POINT('Ctrl Pts',(-2.77573338088225,0.351504794741619,
-0.171239100005331));
#72410=CARTESIAN_POINT('Ctrl Pts',(-1.80933791412281,-2.1375423700464,-0.013244209005277));
#72411=CARTESIAN_POINT('Ctrl Pts',(0.800729748594893,-2.68087948155196,
0.144750681994776));
#72412=CARTESIAN_POINT('Ctrl Pts',(2.68321992772198,-0.795544356782894,
0.30274557299483));
#72413=CARTESIAN_POINT('Ctrl Pts',(2.13222685489998,1.81318819272267,0.460740463994884));
#72414=CARTESIAN_POINT('Ctrl Pts',(-0.353356050373597,2.77617865909866,
0.618735354994938));
#72415=CARTESIAN_POINT('Ctrl Pts',(-2.51821971460423,1.2212058130903,0.77673024599499));
#72416=CARTESIAN_POINT('Ctrl Pts',(-2.39875016986203,-1.44183805604875,
0.934725136995045));
#72417=CARTESIAN_POINT('Ctrl Pts',(-0.103189861818606,-2.79677945469355,
1.0927200279951));
#72418=CARTESIAN_POINT('Ctrl Pts',(2.28595558559378,-1.6146683983646,1.25071491899515));
#72419=CARTESIAN_POINT('Ctrl Pts',(2.60139192527736,1.0322363870214,1.4087098099952));
#72420=CARTESIAN_POINT('Ctrl Pts',(0.556949311928898,2.7427217714679,1.56670470099526));
#72421=CARTESIAN_POINT('Ctrl Pts',(-1.99273057992189,1.96513605211958,1.72469959199531));
#72422=CARTESIAN_POINT('Ctrl Pts',(-2.73469173326279,-0.595142683011921,
1.88269448299537));
#72423=CARTESIAN_POINT('Ctrl Pts',(-0.995855715555496,-2.61553061219188,
2.04068937399542));
#72424=CARTESIAN_POINT('Ctrl Pts',(1.64637781974439,-2.26322161422709,2.19868426499547));
#72425=CARTESIAN_POINT('Ctrl Pts',(2.79508756969503,0.142186649832604,2.35667915599553));
#72426=CARTESIAN_POINT('Ctrl Pts',(1.40821242874264,2.41860884498944,2.51467404699558));
#72427=CARTESIAN_POINT('Ctrl Pts',(-1.25613315819632,2.50097199645567,2.67266893799564));
#72428=CARTESIAN_POINT('Ctrl Pts',(-2.78096812139655,0.314559449318749,
2.83066382899569));
#72429=CARTESIAN_POINT('Ctrl Pts',(-1.78302687496254,-2.15720801874703,
2.98865871999574));
#72430=CARTESIAN_POINT('Ctrl Pts',(0.832400628534772,-2.67204800324426,
3.1466536109958));
#72431=CARTESIAN_POINT('Ctrl Pts',(2.69270963387839,-0.762919488957052,
3.30464850199585));
#72432=CARTESIAN_POINT('Ctrl Pts',(2.11030679852043,1.83829718168443,3.4626433929959));
#72433=CARTESIAN_POINT('Ctrl Pts',(-0.386476751895552,2.77188871376435,
3.62063828399595));
#72434=CARTESIAN_POINT('Ctrl Pts',(-2.53266500493224,1.1909405067813,3.77863317499601));
#72435=CARTESIAN_POINT('Ctrl Pts',(-2.38132711099884,-1.47037835529628,
3.93662806599605));
#72436=CARTESIAN_POINT('Ctrl Pts',(-0.0697503817448946,-2.79783241149437,
4.09462295699612));
#72437=CARTESIAN_POINT('Ctrl Pts',(2.30510093209087,-1.58721170953314,4.25261784799616));
#72438=CARTESIAN_POINT('Ctrl Pts',(2.5888625630092,1.06326005653742,4.41061273899623));
#72439=CARTESIAN_POINT('Ctrl Pts',(0.524118009051023,2.74918744918107,4.56860762999628));
#72440=CARTESIAN_POINT('Ctrl Pts',(-2.01608414683087,1.9411687281004,4.72660252099633));
#72441=CARTESIAN_POINT('Ctrl Pts',(-2.72738037475851,-0.627795834204506,
4.88459741199638));
#72442=CARTESIAN_POINT('Ctrl Pts',(-0.964512940920624,-2.62725067416123,
5.04259230299644));
#72443=CARTESIAN_POINT('Ctrl Pts',(1.67331967629405,-2.24337526486265,5.20058719399648));
#72444=CARTESIAN_POINT('Ctrl Pts',(2.79318773824162,0.175594923072764,5.35858208499656));
#72445=CARTESIAN_POINT('Ctrl Pts',(1.37919449268132,2.43527285317938,5.51657697599659));
#72446=CARTESIAN_POINT('Ctrl Pts',(-1.28594543116668,2.48577466117395,5.67457186699666));
#72447=CARTESIAN_POINT('Ctrl Pts',(-2.78453026564846,0.281287251330417,
5.8325667579967));
#72448=CARTESIAN_POINT('Ctrl Pts',(-1.75710748413146,-2.17837200846936,
5.99056164899676));
#72449=CARTESIAN_POINT('Ctrl Pts',(0.864288593995119,-2.66190468356086,
6.14855653999681));
#72450=CARTESIAN_POINT('Ctrl Pts',(2.70163876039796,-0.730670463607777,
6.30655143099686));
#72451=CARTESIAN_POINT('Ctrl Pts',(2.08817696449889,1.86339697407977,6.46454632199692));
#72452=CARTESIAN_POINT('Ctrl Pts',(-0.419590302218696,2.76706980330411,
6.62254121299697));
#72453=CARTESIAN_POINT('Ctrl Pts',(-2.54672306405081,1.16057440653543,6.78053610399702));
#72454=CARTESIAN_POINT('Ctrl Pts',(-2.3635768050391,-1.49874480975067,6.93853099499709));
#72455=CARTESIAN_POINT('Ctrl Pts',(-0.0362940343214689,-2.79846637663312,
7.09652588599712));
#72456=CARTESIAN_POINT('Ctrl Pts',(2.32391314315961,-1.55953807940794,7.2545207769972));
#72457=CARTESIAN_POINT('Ctrl Pts',(2.57596499873257,1.09413693995685,7.41251566799723));
#72458=CARTESIAN_POINT('Ctrl Pts',(0.491210792034311,2.75525738831465,7.5705105589973));
#72459=CARTESIAN_POINT('Ctrl Pts',(-2.03914898665099,1.91692533196097,7.72850544999735));
#72460=CARTESIAN_POINT('Ctrl Pts',(-2.71967939412015,-0.66035998612245,
7.8865003409974));
#72461=CARTESIAN_POINT('Ctrl Pts',(-0.9330321424437,-2.63859476601473,8.04449523199746));
#72462=CARTESIAN_POINT('Ctrl Pts',(1.70002224901497,-2.22320841823872,8.2024901229975));
#72463=CARTESIAN_POINT('Ctrl Pts',(2.79088864512093,0.208978201275766,8.36048501399757));
#72464=CARTESIAN_POINT('Ctrl Pts',(1.34997937336987,2.45158867054595,8.51847990499762));
#72465=CARTESIAN_POINT('Ctrl Pts',(-1.31557386100644,2.47022200101732,8.67647479599767));
#72466=CARTESIAN_POINT('Ctrl Pts',(-2.78769435259396,0.247974826523285,
8.83446968699772));
#72467=CARTESIAN_POINT('Ctrl Pts',(-1.73093690286391,-2.19922458070505,
8.99246457799778));
#72468=CARTESIAN_POINT('Ctrl Pts',(0.896053003445084,-2.6513808351669,9.15045946899784));
#72469=CARTESIAN_POINT('Ctrl Pts',(2.71018167460651,-0.698316982967359,
9.30845435999788));
#72470=CARTESIAN_POINT('Ctrl Pts',(2.06574861445826,1.88823038317285,9.46644925099794));
#72471=CARTESIAN_POINT('Ctrl Pts',(-0.45264386973844,2.76185532663481,9.62444414199799));
#72472=CARTESIAN_POINT('Ctrl Pts',(-2.5604170561675,1.13004239591331,9.78243903299804));
#72473=CARTESIAN_POINT('Ctrl Pts',(-2.34548861359897,-1.52689701078686,
9.9404339239981));
#72474=CARTESIAN_POINT('Ctrl Pts',(-0.00283249851198579,-2.79870028674429,
10.0984288149982));
#72475=CARTESIAN_POINT('Ctrl Pts',(2.34239313895008,-1.53164150527581,10.2564237059982));
#72476=CARTESIAN_POINT('Ctrl Pts',(2.56269918704329,1.12485741087042,10.4144185969983));
#72477=CARTESIAN_POINT('Ctrl Pts',(0.458233353927178,2.76093344928963,10.5724134879983));
#72478=CARTESIAN_POINT('Ctrl Pts',(-2.06192231968409,1.89240790151988,10.7304083789984));
#72479=CARTESIAN_POINT('Ctrl Pts',(-2.71158962134898,-0.692829736205835,
10.8884032699984));
#72480=CARTESIAN_POINT('Ctrl Pts',(-0.90141796228012,-2.64956165719617,
11.0463981609985));
#72481=CARTESIAN_POINT('Ctrl Pts',(1.72648179491819,-2.20272375262492,11.2043930519985));
#72482=CARTESIAN_POINT('Ctrl Pts',(2.7881905800153,0.242331605070017,11.3623879429986));
#72483=CARTESIAN_POINT('Ctrl Pts',(1.32057126786748,2.46755402056041,11.5203828339987));
#72484=CARTESIAN_POINT('Ctrl Pts',(-1.34501422335496,2.45431621031658,11.6783777249987));
#72485=CARTESIAN_POINT('Ctrl Pts',(-2.79045992331823,0.214626951768239,
11.8363726159988));
#72486=CARTESIAN_POINT('Ctrl Pts',(-1.70451887724915,-2.21976276122321,
11.9943675069988));
#72487=CARTESIAN_POINT('Ctrl Pts',(0.927689321261817,-2.64047796075702,
12.1523623979988));
#72488=CARTESIAN_POINT('Ctrl Pts',(2.71833714731268,-0.66586366962402,12.3103572889989));
#72489=CARTESIAN_POINT('Ctrl Pts',(2.04302496870488,1.91279385105346,12.468352179999));
#72490=CARTESIAN_POINT('Ctrl Pts',(-0.48563275555883,2.75624604578475,12.626347070999));
#72491=CARTESIAN_POINT('Ctrl Pts',(-2.57374497374716,1.09934880708429,12.7843419619991));
#72492=CARTESIAN_POINT('Ctrl Pts',(-2.32706521767492,-1.55483087129818,
12.9423368529991));
#72493=CARTESIAN_POINT('Ctrl Pts',(0.0306296239850783,-2.7985342282319,
13.1003317439992));
#72494=CARTESIAN_POINT('Ctrl Pts',(2.36053793034993,-1.50352574600393,13.2583266349992));
#72495=CARTESIAN_POINT('Ctrl Pts',(2.54906768788899,1.15541663986578,13.4163215259993));
#72496=CARTESIAN_POINT('Ctrl Pts',(0.42518914129335,2.76621565710669,13.5743164169993));
#72497=CARTESIAN_POINT('Ctrl Pts',(-2.08439846825039,1.86761834358563,13.7323113079994));
#72498=CARTESIAN_POINT('Ctrl Pts',(-2.7031168406022,-0.725197389434075,
13.8903061989994));
#72499=CARTESIAN_POINT('Ctrl Pts',(-0.869666078203209,-2.66015561356989,
14.0483010899995));
#72500=CARTESIAN_POINT('Ctrl Pts',(1.75267763866885,-2.18191305067097,14.2062959809995));
#72501=CARTESIAN_POINT('Ctrl Pts',(2.78512620401791,0.275629071355557,14.3642908719996));
#72502=CARTESIAN_POINT('Ctrl Pts',(1.29091271455523,2.48320730756548,14.5222857629997));
#72503=CARTESIAN_POINT('Ctrl Pts',(-1.37414448785656,2.43798182357128,14.6802806539997));
#72504=CARTESIAN_POINT('Ctrl Pts',(-2.79305172314729,0.181396953694044,
14.8382755449998));
#72505=CARTESIAN_POINT('Ctrl Pts',(-1.67742675687761,-2.24026772494819,
14.9962704359998));
#72506=CARTESIAN_POINT('Ctrl Pts',(0.958368222991996,-2.62865236842956,
15.1542653269999));
#72507=CARTESIAN_POINT('Ctrl Pts',(2.7277014223945,-0.634378452891388,15.3122602179999));
#72508=CARTESIAN_POINT('Ctrl Pts',(2.01676643438217,1.93930517753648,15.470255109));
#72509=CARTESIAN_POINT('Ctrl Pts',(0.331786659212352,2.47609764328476,15.5755850363333));
#72510=CARTESIAN_POINT('Ctrl Pts',(-0.439445221994538,2.33068358199181,
15.62825));
#72511=CARTESIAN_POINT('Ctrl Pts',(-1.12236674703448,2.30288577939268,-0.219489327336923));
#72512=CARTESIAN_POINT('Ctrl Pts',(-1.88440023178909,1.93149044095738,-0.166824363670239));
#72513=CARTESIAN_POINT('Ctrl Pts',(-2.99819386511655,0.37967606197771,-0.0614944363368692));
#72514=CARTESIAN_POINT('Ctrl Pts',(-1.9543468660962,-2.30885518920509,0.096500454663184));
#72515=CARTESIAN_POINT('Ctrl Pts',(0.864904041716857,-2.89573792283723,
0.254495345663238));
#72516=CARTESIAN_POINT('Ctrl Pts',(2.89826594350265,-0.859303067925248,
0.412490236663291));
#72517=CARTESIAN_POINT('Ctrl Pts',(2.30311366337569,1.95850572434841,0.570485127663346));
#72518=CARTESIAN_POINT('Ctrl Pts',(-0.381675686047029,2.99867483004853,
0.728480018663398));
#72519=CARTESIAN_POINT('Ctrl Pts',(-2.72004182798788,1.31907905927489,0.886474909663454));
#72520=CARTESIAN_POINT('Ctrl Pts',(-2.59099742531531,-1.55739382028214,
1.0444698006635));
#72521=CARTESIAN_POINT('Ctrl Pts',(-0.111459988476451,-3.02092667145178,
1.20246469166356));
#72522=CARTESIAN_POINT('Ctrl Pts',(2.46916294621846,-1.74407560881646,1.36045958266361));
#72523=CARTESIAN_POINT('Ctrl Pts',(2.80987985548213,1.11496472400166,1.51845447366367));
#72524=CARTESIAN_POINT('Ctrl Pts',(0.60158588058462,2.96253654820512,1.67644936466372));
#72525=CARTESIAN_POINT('Ctrl Pts',(-2.15243749298894,2.12263140839256,1.83444425566377));
#72526=CARTESIAN_POINT('Ctrl Pts',(-2.95386294451934,-0.642840250207365,
1.99243914666383));
#72527=CARTESIAN_POINT('Ctrl Pts',(-1.07566833237088,-2.82515168405898,
2.15043403766388));
#72528=CARTESIAN_POINT('Ctrl Pts',(1.77832637414643,-2.44460696618424,2.30842892866393));
#72529=CARTESIAN_POINT('Ctrl Pts',(3.01909919073696,0.153582164686878,2.46642381966399));
#72530=CARTESIAN_POINT('Ctrl Pts',(1.52107327516274,2.61244766918467,2.62441871066404));
#72531=CARTESIAN_POINT('Ctrl Pts',(-1.35680564805421,2.70141179561648,2.7824136016641));
#72532=CARTESIAN_POINT('Ctrl Pts',(-3.00384814265038,0.339769740731444,
2.94040849266415));
#72533=CARTESIAN_POINT('Ctrl Pts',(-1.92592713503036,-2.33009693659115,
3.0984033836642));
#72534=CARTESIAN_POINT('Ctrl Pts',(0.899113176712534,-2.88619864782458,
3.25639827466426));
#72535=CARTESIAN_POINT('Ctrl Pts',(2.90851619987664,-0.824063487913928,
3.41439316566431));
#72536=CARTESIAN_POINT('Ctrl Pts',(2.27943682934948,1.98562706719167,3.57238805666436));
#72537=CARTESIAN_POINT('Ctrl Pts',(-0.417450838226782,2.99404106807715,
3.73038294766441));
#72538=CARTESIAN_POINT('Ctrl Pts',(-2.73564483263507,1.2863881472707,3.88837783866447));
#72539=CARTESIAN_POINT('Ctrl Pts',(-2.57217799958985,-1.5882214749488,4.04637272966452));
#72540=CARTESIAN_POINT('Ctrl Pts',(-0.0753405093145775,-3.02206401722216,
4.20436762066458));
#72541=CARTESIAN_POINT('Ctrl Pts',(2.48984269190601,-1.71441841026206,4.36236251166463));
#72542=CARTESIAN_POINT('Ctrl Pts',(2.79634633048836,1.1484747780497,4.52035740266469));
#72543=CARTESIAN_POINT('Ctrl Pts',(0.566123320833673,2.9695204161036,4.67835229366474));
#72544=CARTESIAN_POINT('Ctrl Pts',(-2.1776627259012,2.09674322895411,4.83634718466479));
#72545=CARTESIAN_POINT('Ctrl Pts',(-2.94596561894615,-0.678110380349046,
4.99434207566485));
#72546=CARTESIAN_POINT('Ctrl Pts',(-1.04181359860098,-2.83781104757613,
5.1523369666649));
#72547=CARTESIAN_POINT('Ctrl Pts',(1.80742747930962,-2.42317003592312,5.31033185766495));
#72548=CARTESIAN_POINT('Ctrl Pts',(3.01704709774863,0.189667935951029,5.46832674866501));
#72549=CARTESIAN_POINT('Ctrl Pts',(1.48972970359473,2.63044721030322,5.62632163966506));
#72550=CARTESIAN_POINT('Ctrl Pts',(-1.38900721847178,2.68499647355363,5.78431653066512));
#72551=CARTESIAN_POINT('Ctrl Pts',(-3.00769577409666,0.303830950437453,
5.94231142166516));
#72552=CARTESIAN_POINT('Ctrl Pts',(-1.89793044085485,-2.35295710917974,
6.10030631266523));
#72553=CARTESIAN_POINT('Ctrl Pts',(0.933556795495496,-2.87524239422467,
6.25830120366527));
#72554=CARTESIAN_POINT('Ctrl Pts',(2.91816094909363,-0.789229872184075,
6.41629609466533));
#72555=CARTESIAN_POINT('Ctrl Pts',(2.25553340510261,2.01273847641193,6.57429098566538));
#72556=CARTESIAN_POINT('Ctrl Pts',(-0.453218266076613,2.98883594719704,
6.73228587666544));
#72557=CARTESIAN_POINT('Ctrl Pts',(-2.75082957152067,1.25358836322381,6.89028076766548));
#72558=CARTESIAN_POINT('Ctrl Pts',(-2.55300509962799,-1.61886135207317,
7.04827565866555));
#72559=CARTESIAN_POINT('Ctrl Pts',(-0.0392028109733089,-3.02274879134448,
7.20627054966559));
#72560=CARTESIAN_POINT('Ctrl Pts',(2.51016260310644,-1.68452688370611,7.36426544066566));
#72561=CARTESIAN_POINT('Ctrl Pts',(2.78241509402469,1.18182628186475,7.5222603316657));
#72562=CARTESIAN_POINT('Ctrl Pts',(0.530578762823495,2.97607682904918,7.68025522266576));
#72563=CARTESIAN_POINT('Ctrl Pts',(-2.2025760917615,2.07055685166173,7.83825011366581));
#72564=CARTESIAN_POINT('Ctrl Pts',(-2.93764744506665,-0.713284378390626,
7.99624500466586));
#72565=CARTESIAN_POINT('Ctrl Pts',(-1.0078097791014,-2.85006430894292,8.15423989566592));
#72566=CARTESIAN_POINT('Ctrl Pts',(1.83627012329917,-2.40138692222673,8.31223478666596));
#72567=CARTESIAN_POINT('Ctrl Pts',(3.01456374436274,0.225726708956776,8.47022967766603));
#72568=CARTESIAN_POINT('Ctrl Pts',(1.45817314557243,2.64807065492862,8.62822456866608));
#72569=CARTESIAN_POINT('Ctrl Pts',(-1.42101021169528,2.66819734918923,8.78621945966612));
#72570=CARTESIAN_POINT('Ctrl Pts',(-3.01111344602942,0.267848709355943,
8.9442143506662));
#72571=CARTESIAN_POINT('Ctrl Pts',(-1.86966242464576,-2.37548090580212,
9.10220924166623));
#72572=CARTESIAN_POINT('Ctrl Pts',(0.967866955901341,-2.86387511453221,
9.26020413266631));
#72573=CARTESIAN_POINT('Ctrl Pts',(2.92738853310682,-0.754283429618888,
9.41819902366633));
#72574=CARTESIAN_POINT('Ctrl Pts',(2.23130754034209,2.03956215310421,9.57619391466641));
#72575=CARTESIAN_POINT('Ctrl Pts',(-0.488920903815691,2.98320355754919,
9.73418880566644));
#72576=CARTESIAN_POINT('Ctrl Pts',(-2.76562106534208,1.22060937195346,9.89218369666651));
#72577=CARTESIAN_POINT('Ctrl Pts',(-2.53346723443519,-1.64926980449067,
10.0501785876666));
#72578=CARTESIAN_POINT('Ctrl Pts',(-0.00305950842402692,-3.02300144812525,
10.2081734786666));
#72579=CARTESIAN_POINT('Ctrl Pts',(2.53012367371502,-1.65439454534941,10.3661683696667));
#72580=CARTESIAN_POINT('Ctrl Pts',(2.76808609704807,1.21500883753128,10.5241632606667));
#72581=CARTESIAN_POINT('Ctrl Pts',(0.494958355870487,2.98220779656589,10.6821581516668));
#72582=CARTESIAN_POINT('Ctrl Pts',(-2.22717458809345,2.0440744776545,10.8401530426668));
#72583=CARTESIAN_POINT('Ctrl Pts',(-2.92890931940236,-0.748356408785326,
10.9981479336669));
#72584=CARTESIAN_POINT('Ctrl Pts',(-0.973661888071959,-2.86191013898051,
11.1561428246669));
#72585=CARTESIAN_POINT('Ctrl Pts',(1.86485026314516,-2.37926051801397,11.314137715667));
#72586=CARTESIAN_POINT('Ctrl Pts',(3.01164944347811,0.261753213276476,11.472132606667));
#72587=CARTESIAN_POINT('Ctrl Pts',(1.42640813452734,2.66531554408024,11.6301274976671));
#72588=CARTESIAN_POINT('Ctrl Pts',(-1.45281006480367,2.6510167927182,11.7881223886671));
#72589=CARTESIAN_POINT('Ctrl Pts',(-3.01410066275426,0.231828177198969,
11.9461172796672));
#72590=CARTESIAN_POINT('Ctrl Pts',(-1.84112713272175,-2.39766511385838,
12.1041121706673));
#72591=CARTESIAN_POINT('Ctrl Pts',(1.00203875880082,-2.85209843187493,12.2621070616673));
#72592=CARTESIAN_POINT('Ctrl Pts',(2.9361976242116,-0.71922915328282,12.4201019526674));
#72593=CARTESIAN_POINT('Ctrl Pts',(2.20676271346495,2.0660942542105,12.5780968436674));
#72594=CARTESIAN_POINT('Ctrl Pts',(-0.52455367595618,2.97714472223446,12.7360917346675));
#72595=CARTESIAN_POINT('Ctrl Pts',(-2.78001714567073,1.1874558528297,12.8940866256675));
#72596=CARTESIAN_POINT('Ctrl Pts',(-2.51356729987571,-1.67944241753446,
13.0520815166676));
#72597=CARTESIAN_POINT('Ctrl Pts',(0.0330844278327718,-3.02282208089334,
13.2100764076676));
#72598=CARTESIAN_POINT('Ctrl Pts',(2.5497226750577,-1.62402545531265,13.3680712986677));
#72599=CARTESIAN_POINT('Ctrl Pts',(2.75336210467249,1.24801722858484,13.5260661896677));
#72600=CARTESIAN_POINT('Ctrl Pts',(0.459265822762407,2.98791334565805,13.6840610806678));
#72601=CARTESIAN_POINT('Ctrl Pts',(-2.25145208218098,2.01729816656161,13.8420559716679));
#72602=CARTESIAN_POINT('Ctrl Pts',(-2.91975748968037,-0.78331815979697,
14.0000508626679));
#72603=CARTESIAN_POINT('Ctrl Pts',(-0.939365256882179,-2.87335314543991,
14.158045753668));
#72604=CARTESIAN_POINT('Ctrl Pts',(1.893145566493,-2.35678194735699,14.316040644668));
#72605=CARTESIAN_POINT('Ctrl Pts',(3.0083394738034,0.297719296989276,14.4740355356681));
#72606=CARTESIAN_POINT('Ctrl Pts',(1.3943726035929,2.68222336000765,14.6320304266681));
#72607=CARTESIAN_POINT('Ctrl Pts',(-1.4842749673478,2.63337329047569,14.7900253176682));
#72608=CARTESIAN_POINT('Ctrl Pts',(-3.01690018175728,0.195934968921086,
14.9480202086682));
#72609=CARTESIAN_POINT('Ctrl Pts',(-1.81186372087882,-2.41981344296957,
15.1060150996683));
#72610=CARTESIAN_POINT('Ctrl Pts',(1.03517641373175,-2.8393250802945,15.2640099906683));
#72611=CARTESIAN_POINT('Ctrl Pts',(2.94631239686769,-0.685220561427491,
15.4220048816684));
#72612=CARTESIAN_POINT('Ctrl Pts',(2.17839969522424,2.09473032457841,15.5799997726684));
#72613=CARTESIAN_POINT('Ctrl Pts',(0.358377621218746,2.67454389339306,15.6853297000018));
#72614=CARTESIAN_POINT('Ctrl Pts',(-0.474664453622694,2.51747565713054,
15.7379946636685));
#72615=CARTESIAN_POINT('Ctrl Pts',(-1.20564430054385,2.47375567929493,-0.109744663668462));
#72616=CARTESIAN_POINT('Ctrl Pts',(-2.02421927182262,2.0748034881184,-0.057079700001777));
#72617=CARTESIAN_POINT('Ctrl Pts',(-3.22065434935084,0.407847329213798,
0.0482502273315919));
#72618=CARTESIAN_POINT('Ctrl Pts',(-2.09935581806959,-2.48016800836378,
0.206245118331646));
#72619=CARTESIAN_POINT('Ctrl Pts',(0.929078334838823,-3.11059636412251,
0.364240009331699));
#72620=CARTESIAN_POINT('Ctrl Pts',(3.11331195928332,-0.923061779067598,
0.522234900331752));
#72621=CARTESIAN_POINT('Ctrl Pts',(2.4740004718514,2.10382325597413,0.680229791331807));
#72622=CARTESIAN_POINT('Ctrl Pts',(-0.409995321720456,3.2211710009984,0.83822468233186));
#72623=CARTESIAN_POINT('Ctrl Pts',(-2.92186394137152,1.41695230545948,0.996219573331913));
#72624=CARTESIAN_POINT('Ctrl Pts',(-2.78324468076858,-1.67294958451553,
1.15421446433197));
#72625=CARTESIAN_POINT('Ctrl Pts',(-0.119730115134298,-3.24507388821001,
1.31220935533202));
#72626=CARTESIAN_POINT('Ctrl Pts',(2.65237030684314,-1.87348281926831,1.47020424633207));
#72627=CARTESIAN_POINT('Ctrl Pts',(3.0183677856869,1.19769306098192,1.62819913733213));
#72628=CARTESIAN_POINT('Ctrl Pts',(0.646222449240343,3.18235132494235,1.78619402833218));
#72629=CARTESIAN_POINT('Ctrl Pts',(-2.31214440605599,2.28012676466554,1.94418891933223));
#72630=CARTESIAN_POINT('Ctrl Pts',(-3.17303415577589,-0.690537817402807,
2.10218381033229));
#72631=CARTESIAN_POINT('Ctrl Pts',(-1.15548094918627,-3.03477275592607,
2.26017870133234));
#72632=CARTESIAN_POINT('Ctrl Pts',(1.91027492854846,-2.62599231814139,2.4181735923324));
#72633=CARTESIAN_POINT('Ctrl Pts',(3.24311081177889,0.16497767954115,2.57616848333245));
#72634=CARTESIAN_POINT('Ctrl Pts',(1.63393412158284,2.80628649337991,2.7341633743325));
#72635=CARTESIAN_POINT('Ctrl Pts',(-1.45747813791209,2.90185159477728,2.89215826533256));
#72636=CARTESIAN_POINT('Ctrl Pts',(-3.22672816390422,0.364980032144142,
3.05015315633261));
#72637=CARTESIAN_POINT('Ctrl Pts',(-2.06882739509817,-2.50298585443527,
3.20814804733266));
#72638=CARTESIAN_POINT('Ctrl Pts',(0.965825724890286,-3.10034929240489,
3.36614293833272));
#72639=CARTESIAN_POINT('Ctrl Pts',(3.1243227658749,-0.885207486870811,3.52413782933277));
#72640=CARTESIAN_POINT('Ctrl Pts',(2.44856686017853,2.13295695269892,3.68213272033283));
#72641=CARTESIAN_POINT('Ctrl Pts',(-0.448424924558006,3.21619342238995,
3.84012761133287));
#72642=CARTESIAN_POINT('Ctrl Pts',(-2.9386246603379,1.3818357877601,3.99812250233293));
#72643=CARTESIAN_POINT('Ctrl Pts',(-2.76302888818086,-1.70606459460131,
4.15611739333298));
#72644=CARTESIAN_POINT('Ctrl Pts',(-0.0809306368842651,-3.24629562294995,
4.31411228433304));
#72645=CARTESIAN_POINT('Ctrl Pts',(2.67458445172116,-1.84162511099097,4.47210717533309));
#72646=CARTESIAN_POINT('Ctrl Pts',(3.00383009796752,1.23368949956199,4.63010206633314));
#72647=CARTESIAN_POINT('Ctrl Pts',(0.608128632616327,3.18985338302612,4.7880969573332));
#72648=CARTESIAN_POINT('Ctrl Pts',(-2.33924130497153,2.25231772980782,4.94609184833325));
#72649=CARTESIAN_POINT('Ctrl Pts',(-3.16455086313379,-0.728424926493586,
5.10408673933331));
#72650=CARTESIAN_POINT('Ctrl Pts',(-1.11911425628133,-3.04837142099104,
5.26208163033336));
#72651=CARTESIAN_POINT('Ctrl Pts',(1.94153528232519,-2.60296480698359,5.42007652133342));
#72652=CARTESIAN_POINT('Ctrl Pts',(3.24090645725565,0.20374094882929,5.57807141233347));
#72653=CARTESIAN_POINT('Ctrl Pts',(1.60026491450814,2.82562156742707,5.73606630333352));
#72654=CARTESIAN_POINT('Ctrl Pts',(-1.49206900577688,2.8842182859333,5.89406119433358));
#72655=CARTESIAN_POINT('Ctrl Pts',(-3.23086128254485,0.326374649544494,
6.05205608533362));
#72656=CARTESIAN_POINT('Ctrl Pts',(-2.03875339757824,-2.52754220989012,
6.21005097633369));
#72657=CARTESIAN_POINT('Ctrl Pts',(1.00282499699587,-3.08858010488847,6.36804586733373));
#72658=CARTESIAN_POINT('Ctrl Pts',(3.1346831377893,-0.847789280760374,6.52604075833379));
#72659=CARTESIAN_POINT('Ctrl Pts',(2.42288984570632,2.16207997874408,6.68403564933384));
#72660=CARTESIAN_POINT('Ctrl Pts',(-0.486846229934527,3.21060209108997,
6.8420305403339));
#72661=CARTESIAN_POINT('Ctrl Pts',(-2.95493607899053,1.34660231991219,7.00002543133394));
#72662=CARTESIAN_POINT('Ctrl Pts',(-2.74243339421689,-1.73897789439567,
7.15802032233401));
#72663=CARTESIAN_POINT('Ctrl Pts',(-0.042111587625147,-3.24703120605584,
7.31601521333405));
#72664=CARTESIAN_POINT('Ctrl Pts',(2.69641206305327,-1.80951568800428,7.47401010433411));
#72665=CARTESIAN_POINT('Ctrl Pts',(2.98886518931682,1.26951562377266,7.63200499533417));
#72666=CARTESIAN_POINT('Ctrl Pts',(0.56994673361268,3.19689626978371,7.78999988633422));
#72667=CARTESIAN_POINT('Ctrl Pts',(-2.36600319687202,2.2241883713625,7.94799477733426));
#72668=CARTESIAN_POINT('Ctrl Pts',(-3.15561549601314,-0.766208770658805,
8.10598966833433));
#72669=CARTESIAN_POINT('Ctrl Pts',(-1.0825874157591,-3.06153385187112,8.26398455933438));
#72670=CARTESIAN_POINT('Ctrl Pts',(1.97251799758337,-2.57956542621475,8.42197945033443));
#72671=CARTESIAN_POINT('Ctrl Pts',(3.23823884360454,0.242475216637791,8.57997434133449));
#72672=CARTESIAN_POINT('Ctrl Pts',(1.566366917775,2.84455263931128,8.73796923233454));
#72673=CARTESIAN_POINT('Ctrl Pts',(-1.52644656238412,2.86617269736115,8.89596412333459));
#72674=CARTESIAN_POINT('Ctrl Pts',(-3.23453253946489,0.287722592188601,
9.05395901433465));
#72675=CARTESIAN_POINT('Ctrl Pts',(-2.0083879464276,-2.55173723089919,9.21195390533469));
#72676=CARTESIAN_POINT('Ctrl Pts',(1.0396809083576,-3.07636939389751,9.36994879633477));
#72677=CARTESIAN_POINT('Ctrl Pts',(3.14459539160713,-0.810249876270418,
9.5279436873348));
#72678=CARTESIAN_POINT('Ctrl Pts',(2.39686646622593,2.19089392303558,9.68593857833487));
#72679=CARTESIAN_POINT('Ctrl Pts',(-0.525197937892946,3.20455178846357,
9.8439334693349));
#72680=CARTESIAN_POINT('Ctrl Pts',(-2.97082507451666,1.31117634799362,10.001928360335));
#72681=CARTESIAN_POINT('Ctrl Pts',(-2.72144585527141,-1.77164259819448,
10.159923251335));
#72682=CARTESIAN_POINT('Ctrl Pts',(-0.00328651833606387,-3.24730260950622,
10.3179181423351));
#72683=CARTESIAN_POINT('Ctrl Pts',(2.71785420847995,-1.77714758542301,10.4759130333351));
#72684=CARTESIAN_POINT('Ctrl Pts',(2.97347300705285,1.30516026419214,10.6339079243352));
#72685=CARTESIAN_POINT('Ctrl Pts',(0.531683357813799,3.20348214384215,10.7919028153352));
#72686=CARTESIAN_POINT('Ctrl Pts',(-2.39242685650282,2.19574105378912,10.9498977063353));
#72687=CARTESIAN_POINT('Ctrl Pts',(-3.14622901745573,-0.803883081364814,
11.1078925973353));
#72688=CARTESIAN_POINT('Ctrl Pts',(-1.0459058138638,-3.07425862076485,11.2658874883354));
#72689=CARTESIAN_POINT('Ctrl Pts',(2.00321873137213,-2.55579728340303,11.4238823793354));
#72690=CARTESIAN_POINT('Ctrl Pts',(3.23510830694092,0.281174821482934,11.5818772703355));
#72691=CARTESIAN_POINT('Ctrl Pts',(1.5322450011872,2.86307706760007,11.7398721613356));
#72692=CARTESIAN_POINT('Ctrl Pts',(-1.56060590625239,2.84771737511982,11.8978670523356));
#72693=CARTESIAN_POINT('Ctrl Pts',(-3.23774140219028,0.2490294026297,12.0558619433357));
#72694=CARTESIAN_POINT('Ctrl Pts',(-1.97773538819436,-2.57556746649356,
12.2138568343357));
#72695=CARTESIAN_POINT('Ctrl Pts',(1.07638819633982,-3.06371890299285,12.3718517253358));
#72696=CARTESIAN_POINT('Ctrl Pts',(3.15405810111051,-0.772594636941618,
12.5298466163358));
#72697=CARTESIAN_POINT('Ctrl Pts',(2.37050045822502,2.21939465736754,12.6878415073359));
#72698=CARTESIAN_POINT('Ctrl Pts',(-0.563474596353531,3.19804339868417,
12.8458363983359));
#72699=CARTESIAN_POINT('Ctrl Pts',(-2.98628931759431,1.2755628985751,13.003831289336));
#72700=CARTESIAN_POINT('Ctrl Pts',(-2.70006938207651,-1.80405396377073,
13.161826180336));
#72701=CARTESIAN_POINT('Ctrl Pts',(0.0355392316804697,-3.24710993355476,
13.3198210713361));
#72702=CARTESIAN_POINT('Ctrl Pts',(2.73890741976546,-1.74452516462138,13.4778159623361));
#72703=CARTESIAN_POINT('Ctrl Pts',(2.95765652145599,1.3406178173039,13.6358108533362));
#72704=CARTESIAN_POINT('Ctrl Pts',(0.493342504231463,3.20961103420941,13.7938057443362));
#72705=CARTESIAN_POINT('Ctrl Pts',(-2.41850569611158,2.16697798953759,13.9518006353363));
#72706=CARTESIAN_POINT('Ctrl Pts',(-3.13639813875855,-0.841438930159867,
14.1097955263364));
#72707=CARTESIAN_POINT('Ctrl Pts',(-1.00906443556115,-3.08655067730993,
14.2677904173364));
#72708=CARTESIAN_POINT('Ctrl Pts',(2.03361349431715,-2.53165084404301,14.4257853083365));
#72709=CARTESIAN_POINT('Ctrl Pts',(3.23155274358889,0.319809522622996,14.5837801993365));
#72710=CARTESIAN_POINT('Ctrl Pts',(1.49783249263057,2.88123941244982,14.7417750903366));
#72711=CARTESIAN_POINT('Ctrl Pts',(-1.59440544683904,2.8287647573801,14.8997699813366));
#72712=CARTESIAN_POINT('Ctrl Pts',(-3.24074864036727,0.210472984148126,
15.0577648723367));
#72713=CARTESIAN_POINT('Ctrl Pts',(-1.94630068488002,-2.59935916099094,
15.2157597633367));
#72714=CARTESIAN_POINT('Ctrl Pts',(1.1119846044715,-3.04999779215944,15.3737546543368));
#72715=CARTESIAN_POINT('Ctrl Pts',(3.16492337134089,-0.73606266996359,15.5317495453368));
#72716=CARTESIAN_POINT('Ctrl Pts',(2.34003295606631,2.25015547162033,15.6897444363369));
#72717=CARTESIAN_POINT('Ctrl Pts',(0.384968583225142,2.87299014350137,15.7950743636703));
#72718=CARTESIAN_POINT('Ctrl Pts',(-0.50988368525085,2.70426773226927,15.847739327337));
#72719=CARTESIAN_POINT('Ctrl Pts',(-1.28892185405322,2.64462557919718,-2.77555756156289E-16));
#72720=CARTESIAN_POINT('Ctrl Pts',(-2.16403831185614,2.21811653527943,0.0526649636666843));
#72721=CARTESIAN_POINT('Ctrl Pts',(-3.44311483358514,0.436018596449888,
0.157994891000053));
#72722=CARTESIAN_POINT('Ctrl Pts',(-2.24436477004298,-2.65148082752247,
0.315989782000107));
#72723=CARTESIAN_POINT('Ctrl Pts',(0.99325262796079,-3.32545480540779,0.47398467300016));
#72724=CARTESIAN_POINT('Ctrl Pts',(3.32835797506399,-0.986820490209951,
0.631979564000214));
#72725=CARTESIAN_POINT('Ctrl Pts',(2.64488728032712,2.24914078759987,0.789974455000268));
#72726=CARTESIAN_POINT('Ctrl Pts',(-0.438314957393884,3.44366717194826,
0.947969346000321));
#72727=CARTESIAN_POINT('Ctrl Pts',(-3.12368605475517,1.51482555164407,1.10596423700038));
#72728=CARTESIAN_POINT('Ctrl Pts',(-2.97549193622185,-1.78850534874892,
1.26395912800043));
#72729=CARTESIAN_POINT('Ctrl Pts',(-0.128000241792142,-3.46922110496824,
1.42195401900048));
#72730=CARTESIAN_POINT('Ctrl Pts',(2.83557766746782,-2.00289002972017,1.57994891000054));
#72731=CARTESIAN_POINT('Ctrl Pts',(3.22685571589167,1.28042139796218,1.73794380100059));
#72732=CARTESIAN_POINT('Ctrl Pts',(0.690859017896064,3.40216610167957,1.89593869200064));
#72733=CARTESIAN_POINT('Ctrl Pts',(-2.47185131912304,2.43762212093852,2.0539335830007));
#72734=CARTESIAN_POINT('Ctrl Pts',(-3.39220536703243,-0.738235384598252,
2.21192847400075));
#72735=CARTESIAN_POINT('Ctrl Pts',(-1.23529356600166,-3.24439382779317,
2.3699233650008));
#72736=CARTESIAN_POINT('Ctrl Pts',(2.0422234829505,-2.80737767009854,2.52791825600086));
#72737=CARTESIAN_POINT('Ctrl Pts',(3.46712243282082,0.176373194395425,2.68591314700091));
#72738=CARTESIAN_POINT('Ctrl Pts',(1.74679496800295,3.00012531757514,2.84390803800096));
#72739=CARTESIAN_POINT('Ctrl Pts',(-1.55815062776997,3.10229139393809,3.00190292900102));
#72740=CARTESIAN_POINT('Ctrl Pts',(-3.44960818515806,0.390190323556838,
3.15989782000107));
#72741=CARTESIAN_POINT('Ctrl Pts',(-2.21172765516599,-2.67587477227939,
3.31789271100113));
#72742=CARTESIAN_POINT('Ctrl Pts',(1.03253827306805,-3.31449993698521,3.47588760200118));
#72743=CARTESIAN_POINT('Ctrl Pts',(3.34012933187316,-0.946351485827688,
3.63388249300123));
#72744=CARTESIAN_POINT('Ctrl Pts',(2.61769689100758,2.28028683820616,3.79187738400129));
#72745=CARTESIAN_POINT('Ctrl Pts',(-0.479399010889233,3.43834577670275,
3.94987227500134));
#72746=CARTESIAN_POINT('Ctrl Pts',(-3.14160448804072,1.4772834282495,4.1078671660014));
#72747=CARTESIAN_POINT('Ctrl Pts',(-2.95387977677187,-1.82390771425382,
4.26586205700145));
#72748=CARTESIAN_POINT('Ctrl Pts',(-0.0865207644539496,-3.47052722867774,
4.4238569480015));
#72749=CARTESIAN_POINT('Ctrl Pts',(2.85932621153631,-1.96883181171989,4.58185183900155));
#72750=CARTESIAN_POINT('Ctrl Pts',(3.21131386544667,1.31890422107427,4.73984673000161));
#72751=CARTESIAN_POINT('Ctrl Pts',(0.65013394439898,3.41018634994864,4.89784162100166));
#72752=CARTESIAN_POINT('Ctrl Pts',(-2.50081988404187,2.40789223066154,5.05583651200171));
#72753=CARTESIAN_POINT('Ctrl Pts',(-3.38313610732142,-0.77873947263813,
5.21383140300178));
#72754=CARTESIAN_POINT('Ctrl Pts',(-1.19641491396169,-3.25893179440594,
5.37182629400181));
#72755=CARTESIAN_POINT('Ctrl Pts',(2.07564308534076,-2.78275957804407,5.52982118500188));
#72756=CARTESIAN_POINT('Ctrl Pts',(3.46476581676266,0.217813961707557,5.68781607600192));
#72757=CARTESIAN_POINT('Ctrl Pts',(1.71080012542156,3.02079592455092,5.84581096700199));
#72758=CARTESIAN_POINT('Ctrl Pts',(-1.59513079308199,3.08344009831299,6.00380585800203));
#72759=CARTESIAN_POINT('Ctrl Pts',(-3.45402679099304,0.348918348651528,
6.1618007490021));
#72760=CARTESIAN_POINT('Ctrl Pts',(-2.17957635430163,-2.7021273106005,6.31979564000214));
#72761=CARTESIAN_POINT('Ctrl Pts',(1.07209319849625,-3.30191781555228,6.4777905310022));
#72762=CARTESIAN_POINT('Ctrl Pts',(3.35120532648497,-0.906348689336672,
6.63578542200224));
#72763=CARTESIAN_POINT('Ctrl Pts',(2.59024628631004,2.31142148107623,6.79378031300231));
#72764=CARTESIAN_POINT('Ctrl Pts',(-0.520474193792445,3.4323682349829,6.95177520400236));
#72765=CARTESIAN_POINT('Ctrl Pts',(-3.15904258646038,1.43961627660056,7.10977009500241));
#72766=CARTESIAN_POINT('Ctrl Pts',(-2.93186168880579,-1.85909443671817,
7.26776498600247));
#72767=CARTESIAN_POINT('Ctrl Pts',(-0.0450203642769841,-3.47131362076721,
7.42575987700253));
#72768=CARTESIAN_POINT('Ctrl Pts',(2.8826615230001,-1.93450449230244,7.58375476800256));
#72769=CARTESIAN_POINT('Ctrl Pts',(3.19531528460895,1.35720496568057,7.74174965900264));
#72770=CARTESIAN_POINT('Ctrl Pts',(0.609314704401862,3.41771571051825,7.89974455000267));
#72771=CARTESIAN_POINT('Ctrl Pts',(-2.52943030198254,2.37781989106326,8.05773944100274));
#72772=CARTESIAN_POINT('Ctrl Pts',(-3.37358354695964,-0.819133162926983,
8.21573433200278));
#72773=CARTESIAN_POINT('Ctrl Pts',(-1.15736505241679,-3.27300339479932,
8.37372922300284));
#72774=CARTESIAN_POINT('Ctrl Pts',(2.10876587186757,-2.75774393020277,8.53172411400289));
#72775=CARTESIAN_POINT('Ctrl Pts',(3.46191394284634,0.259223724318805,8.68971900500295));
#72776=CARTESIAN_POINT('Ctrl Pts',(1.67456068997757,3.04103462369395,8.847713896003));
#72777=CARTESIAN_POINT('Ctrl Pts',(-1.63188291307296,3.06414804553306,9.00570878700305));
#72778=CARTESIAN_POINT('Ctrl Pts',(-3.45795163290035,0.307596475021262,
9.16370367800311));
#72779=CARTESIAN_POINT('Ctrl Pts',(-2.14711346820945,-2.72799355599627,
9.32169856900316));
#72780=CARTESIAN_POINT('Ctrl Pts',(1.11149486081386,-3.28886367326282,9.47969346000322));
#72781=CARTESIAN_POINT('Ctrl Pts',(3.36180225010744,-0.866216322921951,
9.63768835100326));
#72782=CARTESIAN_POINT('Ctrl Pts',(2.56242539210976,2.34222569296695,9.79568324200333));
#72783=CARTESIAN_POINT('Ctrl Pts',(-0.561474971970195,3.42590001937795,
9.95367813300337));
#72784=CARTESIAN_POINT('Ctrl Pts',(-3.17602908369125,1.40174332403378,10.1116730240034));
#72785=CARTESIAN_POINT('Ctrl Pts',(-2.90942447610763,-1.8940153918983,10.2696679150035));
#72786=CARTESIAN_POINT('Ctrl Pts',(-0.0035135282481055,-3.47160377088719,
10.4276628060035));
#72787=CARTESIAN_POINT('Ctrl Pts',(2.90558474324488,-1.89990062549661,10.5856576970036));
#72788=CARTESIAN_POINT('Ctrl Pts',(3.17885991705762,1.39531169085301,10.7436525880036));
#72789=CARTESIAN_POINT('Ctrl Pts',(0.568408359757113,3.4247564911184,10.9016474790037));
#72790=CARTESIAN_POINT('Ctrl Pts',(-2.55767912491219,2.34740762992373,11.0596423700038));
#72791=CARTESIAN_POINT('Ctrl Pts',(-3.36354871550911,-0.859409753944302,
11.2176372610038));
#72792=CARTESIAN_POINT('Ctrl Pts',(-1.11814973965565,-3.2866071025492,11.3756321520039));
#72793=CARTESIAN_POINT('Ctrl Pts',(2.14158719959911,-2.73233404879208,11.5336270430039));
#72794=CARTESIAN_POINT('Ctrl Pts',(3.45856717040372,0.300596429689395,11.691621934004));
#72795=CARTESIAN_POINT('Ctrl Pts',(1.63808186784707,3.0608385911199,11.849616825004));
#72796=CARTESIAN_POINT('Ctrl Pts',(-1.66840174770112,3.04441795752144,12.0076117160041));
#72797=CARTESIAN_POINT('Ctrl Pts',(-3.46138214162631,0.266230628060431,
12.1656066070041));
#72798=CARTESIAN_POINT('Ctrl Pts',(-2.11434364366697,-2.75346981912873,
12.3236014980042));
#72799=CARTESIAN_POINT('Ctrl Pts',(1.15073763387882,-3.27533937411076,12.4815963890042));
#72800=CARTESIAN_POINT('Ctrl Pts',(3.37191857800943,-0.825960120600417,
12.6395912800043));
#72801=CARTESIAN_POINT('Ctrl Pts',(2.53423820298509,2.37269506052457,12.7975861710043));
#72802=CARTESIAN_POINT('Ctrl Pts',(-0.602395516750883,3.41894207513388,
12.9555810620044));
#72803=CARTESIAN_POINT('Ctrl Pts',(-3.19256148951789,1.3636699443205,13.1135759530045));
#72804=CARTESIAN_POINT('Ctrl Pts',(-2.8865714642773,-1.928665510007,13.2715708440045));
#72805=CARTESIAN_POINT('Ctrl Pts',(0.0379940355281645,-3.4713977862162,
13.4295657350046));
#72806=CARTESIAN_POINT('Ctrl Pts',(2.92809216447323,-1.8650248739301,13.5875606260046));
#72807=CARTESIAN_POINT('Ctrl Pts',(3.16195093823948,1.43321840602296,13.7455555170047));
#72808=CARTESIAN_POINT('Ctrl Pts',(0.527419185700519,3.43130872276077,13.9035504080047));
#72809=CARTESIAN_POINT('Ctrl Pts',(-2.58555931004217,2.31665781251357,14.0615452990048));
#72810=CARTESIAN_POINT('Ctrl Pts',(-3.35303878783672,-0.89955970052277,
14.2195401900048));
#72811=CARTESIAN_POINT('Ctrl Pts',(-1.07876361424012,-3.29974820917995,
14.3775350810049));
#72812=CARTESIAN_POINT('Ctrl Pts',(2.1740814221413,-2.70651974072904,14.5355299720049));
#72813=CARTESIAN_POINT('Ctrl Pts',(3.45476601337439,0.341899748256715,14.693524863005));
#72814=CARTESIAN_POINT('Ctrl Pts',(1.60129238166824,3.08025546489199,14.851519754005));
#72815=CARTESIAN_POINT('Ctrl Pts',(-1.70453592633028,3.02415622428451,15.0095146450051));
#72816=CARTESIAN_POINT('Ctrl Pts',(-3.46459709897726,0.225010999375169,
15.1675095360052));
#72817=CARTESIAN_POINT('Ctrl Pts',(-2.08073764888123,-2.77890487901232,
15.3255044270052));
#72818=CARTESIAN_POINT('Ctrl Pts',(1.18879279521126,-3.26067050402438,15.4834993180053));
#72819=CARTESIAN_POINT('Ctrl Pts',(3.38353434581409,-0.786904778499691,
15.6414942090053));
#72820=CARTESIAN_POINT('Ctrl Pts',(2.50166621690838,2.40558061866225,15.7994891000054));
#72821=CARTESIAN_POINT('Ctrl Pts',(0.411559545231536,3.07143639360967,15.9048190273387));
#72822=CARTESIAN_POINT('Ctrl Pts',(-0.545102916879006,2.891059807408,15.9574839910054));
#72823=CARTESIAN_POINT('Ctrl Pts',(-2.94111188951679,-0.00259486169482749,
14.1778238829104));
#72824=CARTESIAN_POINT('Ctrl Pts',(-2.94335307565858,-0.259762554464039,
14.1917293186085));
#72825=CARTESIAN_POINT('Ctrl Pts',(-2.91238767988341,-0.516399492336486,
14.2056347543067));
#72826=CARTESIAN_POINT('Ctrl Pts',(-2.84607967927153,-0.763554866459577,
14.2195401900048));
#72827=CARTESIAN_POINT('Ctrl Pts',(-2.59494706330453,-1.69962253674182,
14.2722051536715));
#72828=CARTESIAN_POINT('Ctrl Pts',(-1.83685533877235,-2.49968537296086,
14.3248701173382));
#72829=CARTESIAN_POINT('Ctrl Pts',(-0.915668637109368,-2.80084537966192,
14.3775350810049));
#72830=CARTESIAN_POINT('Ctrl Pts',(0.00551806455364026,-3.10200538636298,
14.4302000446716));
#72831=CARTESIAN_POINT('Ctrl Pts',(1.0897997433475,-2.90426256354601,14.4828650083382));
#72832=CARTESIAN_POINT('Ctrl Pts',(1.84538801461659,-2.29732123730656,14.5355299720049));
#72833=CARTESIAN_POINT('Ctrl Pts',(2.60097628588567,-1.6903799110671,14.5881949356716));
#72834=CARTESIAN_POINT('Ctrl Pts',(3.02787114963004,-0.674240081405173,
14.6408598993383));
#72835=CARTESIAN_POINT('Ctrl Pts',(2.93240630955118,0.29022245286501,14.693524863005));
#72836=CARTESIAN_POINT('Ctrl Pts',(2.83694146947232,1.25468498713517,14.7461898266717));
#72837=CARTESIAN_POINT('Ctrl Pts',(2.21911692557029,2.16747022601356,14.7988547903384));
#72838=CARTESIAN_POINT('Ctrl Pts',(1.35923326895286,2.61451297201819,14.851519754005));
#72839=CARTESIAN_POINT('Ctrl Pts',(0.499349612335403,3.06155571802283,14.9041847176717));
#72840=CARTESIAN_POINT('Ctrl Pts',(-0.602593156997484,3.04285597115367,
14.9568496813384));
#72841=CARTESIAN_POINT('Ctrl Pts',(-1.4469080704384,2.56698189356751,15.0095146450051));
#72842=CARTESIAN_POINT('Ctrl Pts',(-1.70601080500511,2.42094600950443,15.0256764300034));
#72843=CARTESIAN_POINT('Ctrl Pts',(-1.94085146734146,2.2318557880317,15.0418382150017));
#72844=CARTESIAN_POINT('Ctrl Pts',(-2.14373220034761,2.01193738948431,15.058));
#72845=CARTESIAN_POINT('Ctrl Pts',(-1.37994859234592,-1.93347131995891,
-1.83880688453542E-16));
#72846=CARTESIAN_POINT('Ctrl Pts',(-1.43831895271373,-1.90176082500493,
-1.96503831907269E-16));
#72847=CARTESIAN_POINT('Ctrl Pts',(-1.49514575458196,-1.86752259046863,
-3.60259795903682E-17));
#72848=CARTESIAN_POINT('Ctrl Pts',(-1.55024291463987,-1.83079524515745,
-1.11022302462516E-16));
#72849=CARTESIAN_POINT('Ctrl Pts',(-1.61820139003649,-1.78549464545158,
-1.89647209120044E-16));
#72850=CARTESIAN_POINT('Ctrl Pts',(-1.68352982136479,-1.73640902813589,
4.37133882625492E-17));
#72851=CARTESIAN_POINT('Ctrl Pts',(-1.74614398662112,-1.68389593204229,
2.08166817117217E-17));
#72852=CARTESIAN_POINT('Ctrl Pts',(-1.78291149355231,-1.65305984859862,
7.3715640875763E-18));
#72853=CARTESIAN_POINT('Ctrl Pts',(-1.81874277362574,-1.62104095184393,
-1.13501056944751E-16));
#72854=CARTESIAN_POINT('Ctrl Pts',(-1.85361742493061,-1.58790418430478,
-1.38777878078145E-16));
#72855=CARTESIAN_POINT('Ctrl Pts',(-1.86599100473682,-1.57614720832583,
-1.47746133009421E-16));
#72856=CARTESIAN_POINT('Ctrl Pts',(-1.87824533378606,-1.56424827137885,
6.18933070998169E-17));
#72857=CARTESIAN_POINT('Ctrl Pts',(-1.89037564784625,-1.55221386701801,
6.93889390390723E-18));
#72858=CARTESIAN_POINT('Ctrl Pts',(-1.9520612058093,-1.49101603289205,-2.72517484859507E-16));
#72859=CARTESIAN_POINT('Ctrl Pts',(-2.01038866542646,-1.42647262579372,
-5.93465220813464E-16));
#72860=CARTESIAN_POINT('Ctrl Pts',(-2.06526482907838,-1.35900295762991,
-3.95516952522712E-16));
#72861=CARTESIAN_POINT('Ctrl Pts',(-2.11328147227381,-1.29996699798658,
-2.22312217768304E-16));
#72862=CARTESIAN_POINT('Ctrl Pts',(-2.15865566139155,-1.2386893890933,-3.33360010116584E-16));
#72863=CARTESIAN_POINT('Ctrl Pts',(-2.20130818996771,-1.17541961668097,
-3.46944695195361E-16));
#72864=CARTESIAN_POINT('Ctrl Pts',(-2.22006840714514,-1.1475911452903,-3.52919760469855E-16));
#72865=CARTESIAN_POINT('Ctrl Pts',(-2.23830186692143,-1.11937693173939,
-3.24730293914024E-16));
#72866=CARTESIAN_POINT('Ctrl Pts',(-2.25600064404541,-1.09079672684346,
-3.05311331771918E-16));
#72867=CARTESIAN_POINT('Ctrl Pts',(-2.26668277274188,-1.07354709288677,
-2.93590982320615E-16));
#72868=CARTESIAN_POINT('Ctrl Pts',(-2.27717011522814,-1.05616412126237,
7.72460434588031E-17));
#72869=CARTESIAN_POINT('Ctrl Pts',(-2.28746078556243,-1.03865201740679,
1.38777878078145E-16));
#72870=CARTESIAN_POINT('Ctrl Pts',(-2.2952947631346,-1.02532057986291,1.85620211640871E-16));
#72871=CARTESIAN_POINT('Ctrl Pts',(-2.30301001735291,-1.01192234024488,
-2.74638834286083E-16));
#72872=CARTESIAN_POINT('Ctrl Pts',(-2.31060459934883,-0.99846213025753,
-2.77555756156289E-16));
#72873=CARTESIAN_POINT('Ctrl Pts',(-2.35418081118604,-0.921230103254969,
-2.94292477860916E-16));
#72874=CARTESIAN_POINT('Ctrl Pts',(-2.39380271969424,-0.841933889485626,
-3.78845217127159E-17));
#72875=CARTESIAN_POINT('Ctrl Pts',(-2.42937389319446,-0.760969916140703,
-6.93889390390723E-17));
#72876=CARTESIAN_POINT('Ctrl Pts',(-2.46720610926394,-0.674859556767564,
-1.02895900045749E-16));
#72877=CARTESIAN_POINT('Ctrl Pts',(-2.5004573035107,-0.586862180324133,
-9.42383278312778E-17));
#72878=CARTESIAN_POINT('Ctrl Pts',(-2.52897137574918,-0.497406668002497,
0.));
#72879=CARTESIAN_POINT('Ctrl Pts',(-2.55035692992803,-0.430315033761271,
7.06787458734584E-17));
#72880=CARTESIAN_POINT('Ctrl Pts',(-2.56907707912655,-0.362402071614612,
2.24154037051898E-16));
#72881=CARTESIAN_POINT('Ctrl Pts',(-2.58504714386116,-0.293835873442853,
2.77555756156289E-16));
#72882=CARTESIAN_POINT('Ctrl Pts',(-2.59702469241211,-0.242411224814034,
3.17607045484582E-16));
#72883=CARTESIAN_POINT('Ctrl Pts',(-2.60745499960513,-0.1906188874626,1.72939271916983E-16));
#72884=CARTESIAN_POINT('Ctrl Pts',(-2.61629539664834,-0.138527206391925,
1.38777878078145E-16));
#72885=CARTESIAN_POINT('Ctrl Pts',(-2.61869711284596,-0.124375191094725,
1.29497076264031E-16));
#72886=CARTESIAN_POINT('Ctrl Pts',(-2.62098183196127,-0.110198515695441,
1.70346493820844E-17));
#72887=CARTESIAN_POINT('Ctrl Pts',(-2.62314735205575,-0.0960068887486099,
2.77555756156289E-17));
#72888=CARTESIAN_POINT('Ctrl Pts',(-2.63712677206149,-0.00439346333649258,
9.69640447732094E-17));
#72889=CARTESIAN_POINT('Ctrl Pts',(-2.64610759043344,0.0876011416361361,
-2.12521409618605E-16));
#72890=CARTESIAN_POINT('Ctrl Pts',(-2.64996359474771,0.179577964648124,
-5.55111512312578E-17));
#72891=CARTESIAN_POINT('Ctrl Pts',(-2.65210628483955,0.230687302523444,
3.17357233945851E-17));
#72892=CARTESIAN_POINT('Ctrl Pts',(-2.65266584064783,0.281791760322423,
2.25858622101648E-16));
#72893=CARTESIAN_POINT('Ctrl Pts',(-2.65161463128253,0.332826444242184,
1.94289029309402E-16));
#72894=CARTESIAN_POINT('Ctrl Pts',(-2.64978728963931,0.421541220055518,
1.40408657934648E-16));
#72895=CARTESIAN_POINT('Ctrl Pts',(-2.6430958113368,0.510044886368098,1.72520161624302E-16));
#72896=CARTESIAN_POINT('Ctrl Pts',(-2.63178393076928,0.598076371345786,
1.66533453693773E-16));
#72897=CARTESIAN_POINT('Ctrl Pts',(-2.62024798910265,0.687851547937211,
1.60428163503557E-16));
#72898=CARTESIAN_POINT('Ctrl Pts',(-2.60390669120625,0.777136386959749,
-1.34425914858345E-16));
#72899=CARTESIAN_POINT('Ctrl Pts',(-2.58296460883121,0.865656938831555,
-1.11022302462516E-16));
#72900=CARTESIAN_POINT('Ctrl Pts',(-2.57869408333521,0.883708117645516,
-1.06249819877211E-16));
#72901=CARTESIAN_POINT('Ctrl Pts',(-2.57423206760738,0.901727502426255,
-4.70036822748448E-17));
#72902=CARTESIAN_POINT('Ctrl Pts',(-2.56958003501042,0.919712740461561,
-5.55111512312578E-17));
#72903=CARTESIAN_POINT('Ctrl Pts',(-2.56604635272843,0.933374320783267,
-6.19734215806574E-17));
#72904=CARTESIAN_POINT('Ctrl Pts',(-2.56240532303519,0.947007284078113,
8.26362614469453E-17));
#72905=CARTESIAN_POINT('Ctrl Pts',(-2.5586586911495,0.960608258314244,8.32667268468867E-17));
#72906=CARTESIAN_POINT('Ctrl Pts',(-2.53407091484386,1.04986648337083,8.74042409382574E-17));
#72907=CARTESIAN_POINT('Ctrl Pts',(-2.504930952964,1.13777933274063,7.81122475311754E-16));
#72908=CARTESIAN_POINT('Ctrl Pts',(-2.47152838793823,1.2240648243653,6.38378239159465E-16));
#72909=CARTESIAN_POINT('Ctrl Pts',(-2.43748524526305,1.31200505589874,4.92896525595146E-16));
#72910=CARTESIAN_POINT('Ctrl Pts',(-2.39901427145562,1.39825569878996,-4.49689980744232E-17));
#72911=CARTESIAN_POINT('Ctrl Pts',(-2.35636659634517,1.48252101187545,-5.55111512312578E-17));
#72912=CARTESIAN_POINT('Ctrl Pts',(-2.31336109209446,1.56749334086406,-6.61417567970626E-17));
#72913=CARTESIAN_POINT('Ctrl Pts',(-2.26610821171127,1.65044775809861,-5.44480906746773E-17));
#72914=CARTESIAN_POINT('Ctrl Pts',(-2.21481327415801,1.731071203515,-5.55111512312578E-17));
#72915=CARTESIAN_POINT('Ctrl Pts',(-2.18401751630642,1.77947481253834,-5.61493770883036E-17));
#72916=CARTESIAN_POINT('Ctrl Pts',(-2.15176385823466,1.82703799978858,3.67516605336294E-16));
#72917=CARTESIAN_POINT('Ctrl Pts',(-2.11808850376184,1.87368930169054,3.88578058618805E-16));
#72918=CARTESIAN_POINT('Ctrl Pts',(-2.1089145366433,1.88639822536441,3.94315699184355E-16));
#72919=CARTESIAN_POINT('Ctrl Pts',(-2.09963412322397,1.89904053530927,1.84615714870052E-16));
#72920=CARTESIAN_POINT('Ctrl Pts',(-2.09025911328956,1.91160012317952,1.66533453693773E-16));
#72921=CARTESIAN_POINT('Ctrl Pts',(-2.03145402967869,1.99038058527982,5.31118266465956E-17));
#72922=CARTESIAN_POINT('Ctrl Pts',(-1.96883756375661,2.06603912302101,4.62847422951145E-16));
#72923=CARTESIAN_POINT('Ctrl Pts',(-1.90268196527442,2.13826743811961,3.33066907387547E-16));
#72924=CARTESIAN_POINT('Ctrl Pts',(-1.83635976195865,2.21067765145044,2.0295955537029E-16));
#72925=CARTESIAN_POINT('Ctrl Pts',(-1.76648017672323,2.2796412428746,3.28001727774597E-18));
#72926=CARTESIAN_POINT('Ctrl Pts',(-1.6932675195623,2.34483179093341,0.));
#72927=CARTESIAN_POINT('Ctrl Pts',(-1.62146081066126,2.40877044429043,-3.21702906282713E-18));
#72928=CARTESIAN_POINT('Ctrl Pts',(-1.54644728359632,2.46908034426641,-8.3280583097932E-18));
#72929=CARTESIAN_POINT('Ctrl Pts',(-1.46839770082455,2.52542611967769,-5.55111512312578E-17));
#72930=CARTESIAN_POINT('Ctrl Pts',(-1.41023968234018,2.56741172077267,-9.06692532072844E-17));
#72931=CARTESIAN_POINT('Ctrl Pts',(-1.35039506896231,2.60719581243537,-1.11866688105539E-17));
#72932=CARTESIAN_POINT('Ctrl Pts',(-1.28892185405323,2.64462557919718,0.));
#72933=CARTESIAN_POINT('Origin',(0.,0.,0.));
#72934=CARTESIAN_POINT('Origin',(-1.44337567297407,-2.5,-6.));
#72935=CARTESIAN_POINT('',(-1.44337567297407,-2.5,-6.));
#72936=CARTESIAN_POINT('',(1.44337567297406,-2.5,-6.));
#72937=CARTESIAN_POINT('',(-0.721687836487033,-2.5,-6.));
#72938=CARTESIAN_POINT('',(-1.44337567297407,-2.5,-3.));
#72939=CARTESIAN_POINT('',(-1.44337567297407,-2.5,-6.));
#72940=CARTESIAN_POINT('',(1.44337567297406,-2.5,-3.));
#72941=CARTESIAN_POINT('',(-1.44337567297407,-2.5,-3.));
#72942=CARTESIAN_POINT('',(1.44337567297406,-2.5,-6.));
#72943=CARTESIAN_POINT('Origin',(-2.88675134594813,3.53525079574969E-16,
-6.));
#72944=CARTESIAN_POINT('',(-2.88675134594813,3.53525079574969E-16,-6.));
#72945=CARTESIAN_POINT('',(-2.52590742770461,-0.625,-6.));
#72946=CARTESIAN_POINT('',(-2.88675134594813,5.55111512312578E-16,-3.));
#72947=CARTESIAN_POINT('',(-2.88675134594813,3.53525079574969E-16,-6.));
#72948=CARTESIAN_POINT('',(-2.88675134594813,3.53525079574969E-16,-3.));
#72949=CARTESIAN_POINT('Origin',(-1.44337567297406,2.5,-6.));
#72950=CARTESIAN_POINT('',(-1.44337567297406,2.5,-6.));
#72951=CARTESIAN_POINT('',(-1.80421959121758,1.875,-6.));
#72952=CARTESIAN_POINT('',(-1.44337567297406,2.5,-3.));
#72953=CARTESIAN_POINT('',(-1.44337567297406,2.5,-6.));
#72954=CARTESIAN_POINT('',(-1.44337567297406,2.5,-3.));
#72955=CARTESIAN_POINT('Origin',(1.44337567297406,2.5,-6.));
#72956=CARTESIAN_POINT('',(1.44337567297406,2.5,-6.));
#72957=CARTESIAN_POINT('',(0.721687836487033,2.5,-6.));
#72958=CARTESIAN_POINT('',(1.44337567297406,2.5,-3.));
#72959=CARTESIAN_POINT('',(1.44337567297406,2.5,-6.));
#72960=CARTESIAN_POINT('',(1.44337567297406,2.5,-3.));
#72961=CARTESIAN_POINT('Origin',(2.88675134594813,0.,-6.));
#72962=CARTESIAN_POINT('',(2.88675134594813,0.,-6.));
#72963=CARTESIAN_POINT('',(2.52590742770461,0.625,-6.));
#72964=CARTESIAN_POINT('',(2.88675134594813,0.,-3.));
#72965=CARTESIAN_POINT('',(2.88675134594813,0.,-6.));
#72966=CARTESIAN_POINT('',(2.88675134594813,0.,-3.));
#72967=CARTESIAN_POINT('Origin',(1.44337567297406,-2.5,-6.));
#72968=CARTESIAN_POINT('',(1.80421959121758,-1.875,-6.));
#72969=CARTESIAN_POINT('',(1.44337567297406,-2.5,-3.));
#72970=CARTESIAN_POINT('Origin',(0.,0.,-3.));
#72971=CARTESIAN_POINT('Origin',(0.,0.,0.));
#72972=CARTESIAN_POINT('',(-5.,-6.12323399573677E-16,0.));
#72973=CARTESIAN_POINT('Origin',(0.,0.,0.));
#72974=CARTESIAN_POINT('Origin',(0.,0.,-6.));
#72975=CARTESIAN_POINT('',(-5.,-6.12323399573677E-16,-6.));
#72976=CARTESIAN_POINT('',(-5.,-6.12323399573677E-16,-6.));
#72977=CARTESIAN_POINT('Origin',(0.,0.,-6.));
#72978=CARTESIAN_POINT('Origin',(0.,0.,-6.));
#72979=CARTESIAN_POINT('Origin',(0.,0.,16.));
#97447=UNCERTAINTY_MEASURE_WITH_UNIT(LENGTH_MEASURE(0.01),#97476,
'DISTANCE_ACCURACY_VALUE',
'Maximum model space distance between geometric entities at asserted c
onnectivities');
#97452=UNCERTAINTY_MEASURE_WITH_UNIT(LENGTH_MEASURE(0.01),#97476,
'DISTANCE_ACCURACY_VALUE',
'Maximum model space distance between geometric entities at asserted c
onnectivities');
#97470=(
GEOMETRIC_REPRESENTATION_CONTEXT(3)
GLOBAL_UNCERTAINTY_ASSIGNED_CONTEXT((#97447))
GLOBAL_UNIT_ASSIGNED_CONTEXT((#97476,#97478,#97479))
REPRESENTATION_CONTEXT('','3D')
);
#97475=(
GEOMETRIC_REPRESENTATION_CONTEXT(3)
GLOBAL_UNCERTAINTY_ASSIGNED_CONTEXT((#97452))
GLOBAL_UNIT_ASSIGNED_CONTEXT((#97476,#97478,#97479))
REPRESENTATION_CONTEXT('','3D')
);
#97476=(
LENGTH_UNIT()
NAMED_UNIT(*)
SI_UNIT(.MILLI.,.METRE.)
);
#97478=(
NAMED_UNIT(*)
PLANE_ANGLE_UNIT()
SI_UNIT($,.RADIAN.)
);
#97479=(
NAMED_UNIT(*)
SI_UNIT($,.STERADIAN.)
SOLID_ANGLE_UNIT()
);
#97497=SHAPE_DEFINITION_REPRESENTATION(#97559,#97620);
#97559=PRODUCT_DEFINITION_SHAPE('',$,#97643);
#97620=SHAPE_REPRESENTATION('',(#22990),#97470);
#97625=PRODUCT_DEFINITION_CONTEXT('part definition',#97693,'design');
#97643=PRODUCT_DEFINITION('Socket head cap screw M6x16',
'Socket head cap screw M6x16',#97665,#97625);
#97665=PRODUCT_DEFINITION_FORMATION('',$,#97712);
#97693=APPLICATION_CONTEXT(
'Core Data for Automotive Mechanical Design Process');
#97694=PRODUCT_CONTEXT('part definition',#97693,'mechanical');
#97712=PRODUCT('Socket head cap screw M6x16',
'Socket head cap screw M6x16',$,(#97694));
#97720=PRESENTATION_STYLE_ASSIGNMENT((#97727));
#97727=SURFACE_STYLE_USAGE(.BOTH.,#97734);
#97734=SURFACE_SIDE_STYLE('',(#97741));
#97741=SURFACE_STYLE_FILL_AREA(#97748);
#97748=FILL_AREA_STYLE('Dark gray',(#97755));
#97755=FILL_AREA_STYLE_COLOUR('Dark gray',#97762);
#97762=COLOUR_RGB('Dark gray',0.250980392156863,0.282352941176471,0.32156862745098);
ENDSEC;
END-ISO-10303-21;
